ISO-10303-21;
HEADER;
FILE_DESCRIPTION (('STEP AP214'),
    '1' );
FILE_NAME ('spur gear_iso_ISO - Spur gear 3M 12T 20PA 5FW ---S12A75H50L10.0S1.step',
    '2026-10-27T08:02:39',
    ( '' ),
    ( '' ),
    'SwSTEP 2.0',
    'SolidWorks 2026',
    '' );
FILE_SCHEMA (( 'AUTOMOTIVE_DESIGN' ));
ENDSEC;

DATA;
#1=CARTESIAN_POINT ( 'NONE',  ( 4.999999999999999112, 8.035066368449411911, -14.88411597386720508 ) ) ;
#8=CYLINDRICAL_SURFACE ( 'NONE', #3786, 14.24900000001425227 ) ;
#11=LINE ( 'NONE', #10463, #885 ) ;
#20=CARTESIAN_POINT ( 'NONE',  ( 0.000000000000000000, 0.000000000000000000, 0.000000000000000000 ) ) ;
#24=AXIS2_PLACEMENT_3D ( 'NONE', #11957, #9116, #6050 ) ;
#26=VERTEX_POINT ( 'NONE', #5218 ) ;
#28=VECTOR ( 'NONE', #1970, 1000.000000000000000 ) ;
#31=VERTEX_POINT ( 'NONE', #9797 ) ;
#34=ORIENTED_EDGE ( 'NONE', *, *, #1883, .F. ) ;
#55=ORIENTED_EDGE ( 'NONE', *, *, #1807, .F. ) ;
#58=DIRECTION ( 'NONE',  ( 0.000000000000000000, 0.000000000000000000, -1.000000000000000000 ) ) ;
#63=EDGE_CURVE ( 'NONE', #1039, #8590, #3790, .T. ) ;
#72=CARTESIAN_POINT ( 'NONE',  ( 0.000000000000000000, -20.13931372320393010, 5.950465759858794002 ) ) ;
#74=EDGE_CURVE ( 'NONE', #10051, #9763, #2189, .T. ) ;
#76=ORIENTED_EDGE ( 'NONE', *, *, #9297, .F. ) ;
#80=CARTESIAN_POINT ( 'NONE',  ( 50.00005079999999680, 0.000000000000000000, 5.000000000000000000 ) ) ;
#85=EDGE_LOOP ( 'NONE', ( #11656, #7986, #6514, #6024 ) ) ;
#86=DIRECTION ( 'NONE',  ( 1.000000000000000000, -0.000000000000000000, -0.000000000000000000 ) ) ;
#107=DIRECTION ( 'NONE',  ( -1.000000000000000000, 0.000000000000000000, -0.000000000000000000 ) ) ;
#109=ORIENTED_EDGE ( 'NONE', *, *, #4761, .F. ) ;
#111=EDGE_LOOP ( 'NONE', ( #11683, #9345, #10603, #11669 ) ) ;
#114=VERTEX_POINT ( 'NONE', #4279 ) ;
#122=DIRECTION ( 'NONE',  ( -1.000000000000000000, 0.000000000000000000, 0.000000000000000000 ) ) ;
#125=EDGE_CURVE ( 'NONE', #9327, #10148, #1383, .T. ) ;
#126=CARTESIAN_POINT ( 'NONE',  ( 0.000000000000000000, 20.13931372320388391, 5.950465759858938775 ) ) ;
#134=LINE ( 'NONE', #5901, #805 ) ;
#136=LINE ( 'NONE', #11503, #10649 ) ;
#139=DIRECTION ( 'NONE',  ( 0.000000000000000000, 0.000000000000000000, 1.000000000000000000 ) ) ;
#141=ORIENTED_EDGE ( 'NONE', *, *, #8217, .F. ) ;
#152=ORIENTED_EDGE ( 'NONE', *, *, #2116, .F. ) ;
#168=DIRECTION ( 'NONE',  ( 0.000000000000000000, 0.000000000000000000, 1.000000000000000000 ) ) ;
#178=DIRECTION ( 'NONE',  ( -1.000000000000000000, 0.000000000000000000, 0.000000000000000000 ) ) ;
#179=DIRECTION ( 'NONE',  ( 0.000000000000000000, 0.000000000000000000, 1.000000000000000000 ) ) ;
#185=VERTEX_POINT ( 'NONE', #1476 ) ;
#202=ORIENTED_EDGE ( 'NONE', *, *, #9372, .F. ) ;
#205=DIRECTION ( 'NONE',  ( 0.000000000000000000, 0.000000000000000000, 1.000000000000000000 ) ) ;
#210=CARTESIAN_POINT ( 'NONE',  ( 4.999999999999999112, -16.90755573046745752, -0.4834863907627537372 ) ) ;
#212=CARTESIAN_POINT ( 'NONE',  ( 0.000000000000000000, 0.000000000000000000, 0.000000000000000000 ) ) ;
#218=CIRCLE ( 'NONE', #406, 7.200000000007204193 ) ;
#223=ORIENTED_EDGE ( 'NONE', *, *, #8092, .T. ) ;
#227=CIRCLE ( 'NONE', #1419, 14.24900000001425227 ) ;
#228=AXIS2_PLACEMENT_3D ( 'NONE', #6814, #4871, #168 ) ;
#229=LINE ( 'NONE', #3922, #9820 ) ;
#230=CYLINDRICAL_SURFACE ( 'NONE', #1227, 7.200000000007202416 ) ;
#235=AXIS2_PLACEMENT_3D ( 'NONE', #1289, #9923, #1479 ) ;
#272=ORIENTED_EDGE ( 'NONE', *, *, #2387, .T. ) ;
#292=CIRCLE ( 'NONE', #1490, 14.24900000001425582 ) ;
#295=EDGE_LOOP ( 'NONE', ( #1962, #11859, #3381, #7606 ) ) ;
#299=FACE_OUTER_BOUND ( 'NONE', #4000, .T. ) ;
#300=CIRCLE ( 'NONE', #2904, 21.00000000002100009 ) ;
#305=EDGE_CURVE ( 'NONE', #9528, #2794, #2709, .T. ) ;
#324=EDGE_CURVE ( 'NONE', #8560, #9094, #3197, .T. ) ;
#332=EDGE_LOOP ( 'NONE', ( #10813, #7816, #4321, #1251 ) ) ;
#348=CARTESIAN_POINT ( 'NONE',  ( 4.999999999999999112, 14.46592441914985905, -15.22291137398907068 ) ) ;
#365=ADVANCED_FACE ( 'NONE', ( #11915 ), #3321, .T. ) ;
#367=AXIS2_PLACEMENT_3D ( 'NONE', #1541, #8125, #8179 ) ;
#383=VECTOR ( 'NONE', #1264, 1000.000000000000000 ) ;
#385=CARTESIAN_POINT ( 'NONE',  ( 2.499999999999998668, 4.916402349214870071, -20.41639017900854469 ) ) ;
#386=CIRCLE ( 'NONE', #11561, 7.200000000007202416 ) ;
#388=CYLINDRICAL_SURFACE ( 'NONE', #4436, 7.200000000007202416 ) ;
#394=VERTEX_POINT ( 'NONE', #4251 ) ;
#397=CIRCLE ( 'NONE', #9396, 7.200000000007201528 ) ;
#401=FACE_OUTER_BOUND ( 'NONE', #670, .T. ) ;
#402=CARTESIAN_POINT ( 'NONE',  ( 0.000000000000000000, -16.90755573046745752, -0.4834863907627537372 ) ) ;
#403=VERTEX_POINT ( 'NONE', #11063 ) ;
#406=AXIS2_PLACEMENT_3D ( 'NONE', #7256, #11054, #2485 ) ;
#407=ORIENTED_EDGE ( 'NONE', *, *, #7533, .T. ) ;
#415=CIRCLE ( 'NONE', #9610, 7.200000000007202416 ) ;
#416=AXIS2_PLACEMENT_3D ( 'NONE', #8285, #1835, #8338 ) ;
#420=VERTEX_POINT ( 'NONE', #12297 ) ;
#435=AXIS2_PLACEMENT_3D ( 'NONE', #4528, #8295, #2526 ) ;
#438=DIRECTION ( 'NONE',  ( 0.000000000000000000, 0.000000000000000000, 1.000000000000000000 ) ) ;
#439=VECTOR ( 'NONE', #9841, 1000.000000000000000 ) ;
#446=DIRECTION ( 'NONE',  ( -1.000000000000000000, -0.000000000000000000, -0.000000000000000000 ) ) ;
#449=EDGE_CURVE ( 'NONE', #4349, #4914, #3593, .T. ) ;
#450=ORIENTED_EDGE ( 'NONE', *, *, #9313, .T. ) ;
#461=CYLINDRICAL_SURFACE ( 'NONE', #12016, 21.00000000002100009 ) ;
#473=DIRECTION ( 'NONE',  ( -1.000000000000000000, 0.000000000000000000, 0.000000000000000000 ) ) ;
#475=VECTOR ( 'NONE', #9225, 1000.000000000000000 ) ;
#487=DIRECTION ( 'NONE',  ( -1.000000000000000000, -0.000000000000000000, 0.000000000000000000 ) ) ;
#490=CARTESIAN_POINT ( 'NONE',  ( 0.000000000000000000, 14.40062958310465469, -8.872489362018239234 ) ) ;
#498=EDGE_CURVE ( 'NONE', #1263, #8559, #8375, .T. ) ;
#499=EDGE_CURVE ( 'NONE', #10309, #3410, #4192, .T. ) ;
#513=( LENGTH_UNIT ( ) NAMED_UNIT ( * ) SI_UNIT ( .MILLI., .METRE. ) );
#522=CARTESIAN_POINT ( 'NONE',  ( 4.999999999999999112, 8.872489362018390224, -14.40062958310456054 ) ) ;
#528=DIRECTION ( 'NONE',  ( 0.000000000000000000, 0.000000000000000000, 1.000000000000000000 ) ) ;
#538=FACE_OUTER_BOUND ( 'NONE', #3304, .T. ) ;
#541=CARTESIAN_POINT ( 'NONE',  ( 0.000000000000000000, 0.000000000000000000, 0.000000000000000000 ) ) ;
#542=VERTEX_POINT ( 'NONE', #11176 ) ;
#547=EDGE_CURVE ( 'NONE', #11485, #10027, #10190, .T. ) ;
#562=CARTESIAN_POINT ( 'NONE',  ( 0.000000000000000000, 8.527191590521072229, 11.41582255376076027 ) ) ;
#566=CIRCLE ( 'NONE', #7566, 21.00000000002100009 ) ;
#570=CARTESIAN_POINT ( 'NONE',  ( 4.999999999999999112, 15.22291137398921990, 14.46592441914969918 ) ) ;
#573=ORIENTED_EDGE ( 'NONE', *, *, #11359, .T. ) ;
#577=DIRECTION ( 'NONE',  ( 0.000000000000000000, 0.000000000000000000, -1.000000000000000000 ) ) ;
#599=CIRCLE ( 'NONE', #7003, 21.00000000002100009 ) ;
#604=ORIENTED_EDGE ( 'NONE', *, *, #12029, .T. ) ;
#607=FILL_AREA_STYLE ('',( #1683 ) ) ;
#611=VERTEX_POINT ( 'NONE', #10688 ) ;
#618=DIRECTION ( 'NONE',  ( 0.000000000000000000, 8.881784197001252323E-16, 1.000000000000000000 ) ) ;
#619=CIRCLE ( 'NONE', #6640, 7.200000000007202416 ) ;
#629=VERTEX_POINT ( 'NONE', #5742 ) ;
#635=VECTOR ( 'NONE', #1004, 1000.000000000000000 ) ;
#641=LINE ( 'NONE', #11202, #11025 ) ;
#647=AXIS2_PLACEMENT_3D ( 'NONE', #6522, #4460, #10094 ) ;
#648=FACE_OUTER_BOUND ( 'NONE', #8532, .T. ) ;
#656=CARTESIAN_POINT ( 'NONE',  ( 2.499999999999999556, 14.46592441914965121, 15.22291137398927141 ) ) ;
#661=VERTEX_POINT ( 'NONE', #4061 ) ;
#667=ORIENTED_EDGE ( 'NONE', *, *, #5254, .F. ) ;
#670=EDGE_LOOP ( 'NONE', ( #4477, #1175, #12160, #8347 ) ) ;
#684=ORIENTED_EDGE ( 'NONE', *, *, #6242, .F. ) ;
#685=DIRECTION ( 'NONE',  ( -1.000000000000000000, -0.000000000000000000, -0.000000000000000000 ) ) ;
#692=CARTESIAN_POINT ( 'NONE',  ( 0.000000000000000000, 5.950465759859149273, -20.13931372320382351 ) ) ;
#694=DIRECTION ( 'NONE',  ( -1.000000000000000000, -0.000000000000000000, 0.000000000000000000 ) ) ;
#705=ORIENTED_EDGE ( 'NONE', *, *, #5884, .T. ) ;
#706=CARTESIAN_POINT ( 'NONE',  ( 4.999999999999999112, 0.000000000000000000, 0.000000000000000000 ) ) ;
#707=AXIS2_PLACEMENT_3D ( 'NONE', #6696, #7558, #9442 ) ;
#711=EDGE_CURVE ( 'NONE', #8590, #2532, #9562, .T. ) ;
#714=CARTESIAN_POINT ( 'NONE',  ( 0.000000000000000000, 5.950465759858868608, 20.13931372320390523 ) ) ;
#721=CARTESIAN_POINT ( 'NONE',  ( 4.999999999999999112, -20.13931372320384128, -5.950465759859079995 ) ) ;
#725=EDGE_CURVE ( 'NONE', #185, #9803, #1207, .T. ) ;
#732=CYLINDRICAL_SURFACE ( 'NONE', #1380, 7.200000000007202416 ) ;
#740=DIRECTION ( 'NONE',  ( 0.000000000000000000, -0.4999999999999889533, -0.8660254037844451469 ) ) ;
#743=DIRECTION ( 'NONE',  ( -1.000000000000000000, 0.000000000000000000, 0.000000000000000000 ) ) ;
#764=CIRCLE ( 'NONE', #11939, 7.200000000007202416 ) ;
#773=ORIENTED_EDGE ( 'NONE', *, *, #711, .F. ) ;
#774=DIRECTION ( 'NONE',  ( -1.000000000000000000, 0.000000000000000000, -0.000000000000000000 ) ) ;
#779=CARTESIAN_POINT ( 'NONE',  ( 4.999999999999999112, -0.4834863907626938961, 16.90755573046746107 ) ) ;
#797=DIRECTION ( 'NONE',  ( 0.000000000000000000, 0.000000000000000000, 1.000000000000000000 ) ) ;
#801=EDGE_LOOP ( 'NONE', ( #10590, #9547, #9131, #11331 ) ) ;
#803=DIRECTION ( 'NONE',  ( -1.000000000000000000, 0.000000000000000000, 0.000000000000000000 ) ) ;
#804=EDGE_CURVE ( 'NONE', #2076, #10859, #397, .T. ) ;
#805=VECTOR ( 'NONE', #2259, 1000.000000000000000 ) ;
#821=ORIENTED_EDGE ( 'NONE', *, *, #2283, .F. ) ;
#823=DIRECTION ( 'NONE',  ( 0.000000000000000000, 1.000000000000000000, 3.491481338843133355E-15 ) ) ;
#826=DIRECTION ( 'NONE',  ( 0.000000000000000000, 0.000000000000000000, 1.000000000000000000 ) ) ;
#828=VECTOR ( 'NONE', #8616, 1000.000000000000000 ) ;
#830=CARTESIAN_POINT ( 'NONE',  ( 0.000000000000000000, -16.90755573046745752, -0.4834863907627537372 ) ) ;
#836=CIRCLE ( 'NONE', #7636, 21.00000000002100009 ) ;
#841=AXIS2_PLACEMENT_3D ( 'NONE', #8106, #3340, #7915 ) ;
#859=DIRECTION ( 'NONE',  ( -1.000000000000000000, -0.000000000000000000, 0.000000000000000000 ) ) ;
#862=DIRECTION ( 'NONE',  ( -1.000000000000000000, 0.000000000000000000, 0.000000000000000000 ) ) ;
#866=VERTEX_POINT ( 'NONE', #8127 ) ;
#867=FACE_OUTER_BOUND ( 'NONE', #2412, .T. ) ;
#869=AXIS2_PLACEMENT_3D ( 'NONE', #8640, #3886, #11494 ) ;
#870=DIRECTION ( 'NONE',  ( 0.000000000000000000, 0.000000000000000000, -1.000000000000000000 ) ) ;
#876=DIRECTION ( 'NONE',  ( -1.000000000000000000, 0.000000000000000000, 0.000000000000000000 ) ) ;
#879=LINE ( 'NONE', #8202, #4628 ) ;
#885=VECTOR ( 'NONE', #86, 1000.000000000000000 ) ;
#888=DIRECTION ( 'NONE',  ( -1.000000000000000000, -0.000000000000000000, 0.000000000000000000 ) ) ;
#894=DIRECTION ( 'NONE',  ( -1.000000000000000000, 0.000000000000000000, 0.000000000000000000 ) ) ;
#896=LINE ( 'NONE', #2903, #4889 ) ;
#897=UNCERTAINTY_MEASURE_WITH_UNIT (LENGTH_MEASURE( 1.000000000000000082E-05 ), #10067, 'distance_accuracy_value', 'NONE');
#901=APPLICATION_CONTEXT ( 'automotive_design' ) ;
#917=ORIENTED_EDGE ( 'NONE', *, *, #305, .F. ) ;
#928=ORIENTED_EDGE ( 'NONE', *, *, #2879, .F. ) ;
#929=LINE ( 'NONE', #8563, #1357 ) ;
#931=CARTESIAN_POINT ( 'NONE',  ( 0.000000000000000000, -14.14998813191268390, -1.676853263448035536 ) ) ;
#932=CARTESIAN_POINT ( 'NONE',  ( 0.000000000000000000, -14.46592441914954286, -15.22291137398937089 ) ) ;
#933=EDGE_LOOP ( 'NONE', ( #2044, #3069, #11821, #10973 ) ) ;
#940=ORIENTED_EDGE ( 'NONE', *, *, #499, .T. ) ;
#946=EDGE_CURVE ( 'NONE', #2151, #1926, #10200, .T. ) ;
#952=ORIENTED_EDGE ( 'NONE', *, *, #7096, .F. ) ;
#975=CARTESIAN_POINT ( 'NONE',  ( 4.999999999999997335, 6.123233995736766282E-16, -5.000000000000000000 ) ) ;
#976=LINE ( 'NONE', #5872, #2034 ) ;
#989=EDGE_LOOP ( 'NONE', ( #76, #684, #3610, #12217 ) ) ;
#996=CARTESIAN_POINT ( 'NONE',  ( 4.999999999999999112, 20.13931372320388391, 5.950465759858937886 ) ) ;
#1002=DIRECTION ( 'NONE',  ( 0.000000000000000000, 0.000000000000000000, -1.000000000000000000 ) ) ;
#1004=DIRECTION ( 'NONE',  ( -1.000000000000000000, 0.000000000000000000, -0.000000000000000000 ) ) ;
#1013=CARTESIAN_POINT ( 'NONE',  ( 4.999999999999999112, -14.88411597386734897, 8.035066368449154339 ) ) ;
#1018=ORIENTED_EDGE ( 'NONE', *, *, #2208, .F. ) ;
#1023=EDGE_CURVE ( 'NONE', #3084, #9327, #218, .T. ) ;
#1027=EDGE_CURVE ( 'NONE', #2572, #1109, #3415, .T. ) ;
#1029=CARTESIAN_POINT ( 'NONE',  ( 4.999999999999999112, 14.14998813191269633, -1.676853263447935394 ) ) ;
#1036=ORIENTED_EDGE ( 'NONE', *, *, #10914, .T. ) ;
#1037=DIRECTION ( 'NONE',  ( -1.000000000000000000, 0.000000000000000000, 0.000000000000000000 ) ) ;
#1039=VERTEX_POINT ( 'NONE', #975 ) ;
#1048=ADVANCED_FACE ( 'NONE', ( #1157 ), #11418, .T. ) ;
#1049=DIRECTION ( 'NONE',  ( 0.000000000000000000, 0.000000000000000000, -1.000000000000000000 ) ) ;
#1050=DIRECTION ( 'NONE',  ( 0.000000000000000000, 0.8660254037844363761, 0.5000000000000041078 ) ) ;
#1052=ORIENTED_EDGE ( 'NONE', *, *, #498, .T. ) ;
#1056=ORIENTED_EDGE ( 'NONE', *, *, #5802, .T. ) ;
#1057=AXIS2_PLACEMENT_3D ( 'NONE', #11802, #4068, #4995 ) ;
#1058=VECTOR ( 'NONE', #3273, 1000.000000000000000 ) ;
#1060=DIRECTION ( 'NONE',  ( -1.000000000000000000, 0.000000000000000000, 0.000000000000000000 ) ) ;
#1079=DIRECTION ( 'NONE',  ( -1.000000000000000000, 0.000000000000000000, -0.000000000000000000 ) ) ;
#1080=SHAPE_REPRESENTATION ( 'spur gear_iso_ISO - Spur gear 3M 12T 20PA 5FW ---S12A75H50L10.0S1', ( #6056 ), #6434 ) ;
#1081=DIRECTION ( 'NONE',  ( 0.000000000000000000, 0.000000000000000000, 1.000000000000000000 ) ) ;
#1090=CYLINDRICAL_SURFACE ( 'NONE', #4198, 5.000000000000000000 ) ;
#1091=DIRECTION ( 'NONE',  ( -1.000000000000000000, -0.000000000000000000, -0.000000000000000000 ) ) ;
#1108=CARTESIAN_POINT ( 'NONE',  ( -10.00000000000000000, 0.000000000000000000, 0.000000000000000000 ) ) ;
#1109=VERTEX_POINT ( 'NONE', #3735 ) ;
#1114=ORIENTED_EDGE ( 'NONE', *, *, #7913, .T. ) ;
#1117=EDGE_LOOP ( 'NONE', ( #5523, #7085, #2430, #10564 ) ) ;
#1124=EDGE_LOOP ( 'NONE', ( #11736, #5228, #9752, #573 ) ) ;
#1127=LINE ( 'NONE', #4997, #6703 ) ;
#1130=EDGE_CURVE ( 'NONE', #4691, #8601, #5008, .T. ) ;
#1131=PRODUCT_DEFINITION_SHAPE ( 'NONE', 'NONE',  #7402 ) ;
#1133=LINE ( 'NONE', #3946, #10395 ) ;
#1137=DIRECTION ( 'NONE',  ( 0.000000000000000000, 0.000000000000000000, -1.000000000000000000 ) ) ;
#1154=DIRECTION ( 'NONE',  ( 0.000000000000000000, 0.000000000000000000, 1.000000000000000000 ) ) ;
#1157=FACE_OUTER_BOUND ( 'NONE', #8222, .T. ) ;
#1165=CARTESIAN_POINT ( 'NONE',  ( 0.000000000000000000, 0.000000000000000000, 0.000000000000000000 ) ) ;
#1175=ORIENTED_EDGE ( 'NONE', *, *, #11942, .T. ) ;
#1178=ORIENTED_EDGE ( 'NONE', *, *, #5787, .T. ) ;
#1186=AXIS2_PLACEMENT_3D ( 'NONE', #11628, #9942, #3140 ) ;
#1194=ADVANCED_FACE ( 'NONE', ( #5046 ), #8925, .T. ) ;
#1205=EDGE_CURVE ( 'NONE', #8601, #11755, #1409, .T. ) ;
#1207=CIRCLE ( 'NONE', #8399, 7.200000000007202416 ) ;
#1210=CARTESIAN_POINT ( 'NONE',  ( 4.999999999999999112, 14.88411597386729213, 8.035066368449255592 ) ) ;
#1212=ORIENTED_EDGE ( 'NONE', *, *, #3860, .F. ) ;
#1217=VERTEX_POINT ( 'NONE', #7980 ) ;
#1222=AXIS2_PLACEMENT_3D ( 'NONE', #2107, #1985, #1049 ) ;
#1227=AXIS2_PLACEMENT_3D ( 'NONE', #4048, #5927, #7621 ) ;
#1230=DIRECTION ( 'NONE',  ( -1.000000000000000000, 0.000000000000000000, 0.000000000000000000 ) ) ;
#1236=DIRECTION ( 'NONE',  ( 0.000000000000000000, 0.000000000000000000, 1.000000000000000000 ) ) ;
#1242=CIRCLE ( 'NONE', #7251, 7.200000000007201528 ) ;
#1249=LINE ( 'NONE', #5067, #4493 ) ;
#1251=ORIENTED_EDGE ( 'NONE', *, *, #4168, .T. ) ;
#1256=EDGE_CURVE ( 'NONE', #8750, #9748, #3233, .T. ) ;
#1260=CARTESIAN_POINT ( 'NONE',  ( 4.999999999999999112, -15.22291137398912397, -14.46592441914980576 ) ) ;
#1262=DIRECTION ( 'NONE',  ( -1.000000000000000000, 0.000000000000000000, 0.000000000000000000 ) ) ;
#1263=VERTEX_POINT ( 'NONE', #4281 ) ;
#1264=DIRECTION ( 'NONE',  ( 1.000000000000000000, -0.000000000000000000, 0.000000000000000000 ) ) ;
#1272=EDGE_CURVE ( 'NONE', #4406, #9587, #10993, .T. ) ;
#1274=CIRCLE ( 'NONE', #4467, 7.200000000007204193 ) ;
#1277=CARTESIAN_POINT ( 'NONE',  ( 0.000000000000000000, 4.769696007084728073, 1.500000000000000000 ) ) ;
#1289=CARTESIAN_POINT ( 'NONE',  ( -10.00000000000000000, 0.000000000000000000, 0.000000000000000000 ) ) ;
#1290=CARTESIAN_POINT ( 'NONE',  ( 4.999999999999999112, 0.000000000000000000, 0.000000000000000000 ) ) ;
#1297=CARTESIAN_POINT ( 'NONE',  ( 4.999999999999999112, 0.000000000000000000, 0.000000000000000000 ) ) ;
#1319=CYLINDRICAL_SURFACE ( 'NONE', #1431, 7.200000000007202416 ) ;
#1323=FACE_OUTER_BOUND ( 'NONE', #4345, .T. ) ;
#1324=CARTESIAN_POINT ( 'NONE',  ( 4.999999999999999112, -8.527191590521155717, 11.41582255376070343 ) ) ;
#1333=VERTEX_POINT ( 'NONE', #2658 ) ;
#1339=CARTESIAN_POINT ( 'NONE',  ( 0.000000000000000000, 16.90755573046746107, -0.4834863907626340551 ) ) ;
#1340=CARTESIAN_POINT ( 'NONE',  ( 4.999999999999999112, -8.527191590521155717, 11.41582255376070343 ) ) ;
#1357=VECTOR ( 'NONE', #5618, 1000.000000000000000 ) ;
#1360=AXIS2_PLACEMENT_3D ( 'NONE', #1518, #7397, #1701 ) ;
#1365=VECTOR ( 'NONE', #10802, 1000.000000000000000 ) ;
#1371=CARTESIAN_POINT ( 'NONE',  ( 4.999999999999999112, -20.41639017900862996, 4.916402349214511247 ) ) ;
#1374=FACE_BOUND ( 'NONE', #7631, .T. ) ;
#1380=AXIS2_PLACEMENT_3D ( 'NONE', #5498, #2540, #4425 ) ;
#1383=CIRCLE ( 'NONE', #10367, 14.24900000001425582 ) ;
#1384=CIRCLE ( 'NONE', #12155, 7.200000000007202416 ) ;
#1386=CARTESIAN_POINT ( 'NONE',  ( 4.999999999999999112, -1.676853263447986242, 14.14998813191269100 ) ) ;
#1396=AXIS2_PLACEMENT_3D ( 'NONE', #10523, #4715, #4770 ) ;
#1409=CIRCLE ( 'NONE', #1619, 7.200000000007201528 ) ;
#1419=AXIS2_PLACEMENT_3D ( 'NONE', #10858, #1230, #5105 ) ;
#1426=ORIENTED_EDGE ( 'NONE', *, *, #4016, .T. ) ;
#1429=AXIS2_PLACEMENT_3D ( 'NONE', #4339, #8060, #11774 ) ;
#1431=AXIS2_PLACEMENT_3D ( 'NONE', #7204, #3149, #9844 ) ;
#1441=VECTOR ( 'NONE', #9727, 1000.000000000000000 ) ;
#1450=ORIENTED_EDGE ( 'NONE', *, *, #11721, .T. ) ;
#1453=LINE ( 'NONE', #6137, #3433 ) ;
#1474=EDGE_LOOP ( 'NONE', ( #4560, #11323, #11816, #11431 ) ) ;
#1475=VECTOR ( 'NONE', #803, 1000.000000000000000 ) ;
#1476=CARTESIAN_POINT ( 'NONE',  ( 4.999999999999999112, -1.676853263447787068, -14.14998813191271410 ) ) ;
#1479=DIRECTION ( 'NONE',  ( 0.000000000000000000, 0.000000000000000000, 1.000000000000000000 ) ) ;
#1482=AXIS2_PLACEMENT_3D ( 'NONE', #522, #7226, #11143 ) ;
#1490=AXIS2_PLACEMENT_3D ( 'NONE', #5654, #5711, #9588 ) ;
#1496=EDGE_CURVE ( 'NONE', #8928, #3677, #566, .T. ) ;
#1498=DIRECTION ( 'NONE',  ( 0.000000000000000000, 0.000000000000000000, -1.000000000000000000 ) ) ;
#1506=CARTESIAN_POINT ( 'NONE',  ( 4.999999999999999112, -14.40062958310459251, -8.872489362018340486 ) ) ;
#1518=CARTESIAN_POINT ( 'NONE',  ( 0.000000000000000000, 0.000000000000000000, 0.000000000000000000 ) ) ;
#1519=EDGE_CURVE ( 'NONE', #31, #5277, #9169, .T. ) ;
#1526=ORIENTED_EDGE ( 'NONE', *, *, #3195, .T. ) ;
#1530=CARTESIAN_POINT ( 'NONE',  ( 0.000000000000000000, 8.527191590521233877, -11.41582255376064126 ) ) ;
#1532=DIRECTION ( 'NONE',  ( -1.000000000000000000, 0.000000000000000000, 0.000000000000000000 ) ) ;
#1541=CARTESIAN_POINT ( 'NONE',  ( 4.999999999999999112, 0.000000000000000000, 0.000000000000000000 ) ) ;
#1554=EDGE_CURVE ( 'NONE', #1926, #8328, #9361, .T. ) ;
#1555=CARTESIAN_POINT ( 'NONE',  ( 0.000000000000000000, 0.4834863907625768231, 16.90755573046746463 ) ) ;
#1560=EDGE_LOOP ( 'NONE', ( #8739, #10370, #2728, #4669 ) ) ;
#1567=CARTESIAN_POINT ( 'NONE',  ( 0.000000000000000000, -14.40062958310459251, -8.872489362018340486 ) ) ;
#1568=AXIS2_PLACEMENT_3D ( 'NONE', #9560, #4985, #5990 ) ;
#1569=AXIS2_PLACEMENT_3D ( 'NONE', #10691, #10741, #9882 ) ;
#1570=EDGE_CURVE ( 'NONE', #5745, #2177, #11460, .T. ) ;
#1574=CARTESIAN_POINT ( 'NONE',  ( 0.000000000000000000, -8.872489362018288972, 14.40062958310462271 ) ) ;
#1580=DIRECTION ( 'NONE',  ( 0.000000000000000000, 0.000000000000000000, 1.000000000000000000 ) ) ;
#1584=ORIENTED_EDGE ( 'NONE', *, *, #4095, .F. ) ;
#1592=DIRECTION ( 'NONE',  ( 0.000000000000000000, 0.000000000000000000, 1.000000000000000000 ) ) ;
#1600=VECTOR ( 'NONE', #9532, 1000.000000000000000 ) ;
#1604=AXIS2_PLACEMENT_3D ( 'NONE', #9480, #11648, #2959 ) ;
#1606=DIRECTION ( 'NONE',  ( 0.000000000000000000, -0.8660254037844433705, 0.4999999999999920064 ) ) ;
#1609=VERTEX_POINT ( 'NONE', #7912 ) ;
#1612=SURFACE_SIDE_STYLE ('',( #8312 ) ) ;
#1616=CIRCLE ( 'NONE', #3424, 21.00000000002100009 ) ;
#1619=AXIS2_PLACEMENT_3D ( 'NONE', #1339, #6229, #8116 ) ;
#1624=CIRCLE ( 'NONE', #7229, 7.200000000007203305 ) ;
#1638=AXIS2_PLACEMENT_3D ( 'NONE', #5013, #4081, #7904 ) ;
#1642=DIRECTION ( 'NONE',  ( 0.000000000000000000, 0.000000000000000000, -1.000000000000000000 ) ) ;
#1647=CIRCLE ( 'NONE', #7850, 21.00000000002100009 ) ;
#1649=EDGE_CURVE ( 'NONE', #629, #5118, #5088, .T. ) ;
#1671=AXIS2_PLACEMENT_3D ( 'NONE', #4478, #5537, #8300 ) ;
#1680=EDGE_CURVE ( 'NONE', #3401, #3546, #2275, .T. ) ;
#1681=FACE_OUTER_BOUND ( 'NONE', #85, .T. ) ;
#1683=FILL_AREA_STYLE_COLOUR ( '', #8042 ) ;
#1685=CIRCLE ( 'NONE', #1482, 7.200000000007202416 ) ;
#1701=DIRECTION ( 'NONE',  ( 0.000000000000000000, 0.000000000000000000, 1.000000000000000000 ) ) ;
#1703=ORIENTED_EDGE ( 'NONE', *, *, #10738, .F. ) ;
#1704=DIRECTION ( 'NONE',  ( 0.000000000000000000, 0.8660254037844398178, -0.4999999999999980016 ) ) ;
#1708=DIRECTION ( 'NONE',  ( -1.000000000000000000, 0.000000000000000000, -0.000000000000000000 ) ) ;
#1723=VERTEX_POINT ( 'NONE', #4268 ) ;
#1734=EDGE_CURVE ( 'NONE', #4584, #4691, #3168, .T. ) ;
#1741=DIRECTION ( 'NONE',  ( 0.000000000000000000, 0.5000000000000011102, -0.8660254037844380415 ) ) ;
#1744=DIRECTION ( 'NONE',  ( -1.000000000000000000, -0.000000000000000000, -0.000000000000000000 ) ) ;
#1757=FACE_OUTER_BOUND ( 'NONE', #989, .T. ) ;
#1764=AXIS2_PLACEMENT_3D ( 'NONE', #10362, #11432, #58 ) ;
#1766=CARTESIAN_POINT ( 'NONE',  ( 0.000000000000000000, 13.09267581720866858, 5.622796541391611669 ) ) ;
#1802=DIRECTION ( 'NONE',  ( -0.000000000000000000, 0.000000000000000000, 1.000000000000000000 ) ) ;
#1807=EDGE_CURVE ( 'NONE', #11522, #11746, #4154, .T. ) ;
#1821=EDGE_CURVE ( 'NONE', #11485, #26, #11199, .T. ) ;
#1823=CIRCLE ( 'NONE', #12195, 14.24900000001425049 ) ;
#1829=ORIENTED_EDGE ( 'NONE', *, *, #2583, .T. ) ;
#1835=DIRECTION ( 'NONE',  ( -1.000000000000000000, -0.000000000000000000, -0.000000000000000000 ) ) ;
#1836=ADVANCED_FACE ( 'NONE', ( #5333 ), #3463, .T. ) ;
#1839=DIRECTION ( 'NONE',  ( 0.000000000000000000, 0.000000000000000000, -1.000000000000000000 ) ) ;
#1862=VECTOR ( 'NONE', #8140, 1000.000000000000000 ) ;
#1883=EDGE_CURVE ( 'NONE', #5118, #2796, #7109, .T. ) ;
#1885=ORIENTED_EDGE ( 'NONE', *, *, #9478, .F. ) ;
#1888=DIRECTION ( 'NONE',  ( -1.000000000000000000, -0.000000000000000000, 0.000000000000000000 ) ) ;
#1897=DIRECTION ( 'NONE',  ( 0.000000000000000000, 0.000000000000000000, -1.000000000000000000 ) ) ;
#1898=ADVANCED_FACE ( 'NONE', ( #9577 ), #5704, .T. ) ;
#1912=AXIS2_PLACEMENT_3D ( 'NONE', #1574, #10202, #1642 ) ;
#1926=VERTEX_POINT ( 'NONE', #4646 ) ;
#1956=ORIENTED_EDGE ( 'NONE', *, *, #3141, .T. ) ;
#1958=CARTESIAN_POINT ( 'NONE',  ( 4.999999999999999112, 0.000000000000000000, 0.000000000000000000 ) ) ;
#1962=ORIENTED_EDGE ( 'NONE', *, *, #8267, .T. ) ;
#1965=ADVANCED_FACE ( 'NONE', ( #1757 ), #7518, .T. ) ;
#1970=DIRECTION ( 'NONE',  ( -1.000000000000000000, 0.000000000000000000, 0.000000000000000000 ) ) ;
#1985=DIRECTION ( 'NONE',  ( -1.000000000000000000, -0.000000000000000000, -0.000000000000000000 ) ) ;
#1990=CIRCLE ( 'NONE', #5776, 7.200000000007203305 ) ;
#1997=AXIS2_PLACEMENT_3D ( 'NONE', #7585, #7663, #3835 ) ;
#2004=DIRECTION ( 'NONE',  ( -1.000000000000000000, 0.000000000000000000, -0.000000000000000000 ) ) ;
#2016=AXIS2_PLACEMENT_3D ( 'NONE', #6308, #5360, #1606 ) ;
#2034=VECTOR ( 'NONE', #3055, 1000.000000000000000 ) ;
#2044=ORIENTED_EDGE ( 'NONE', *, *, #10522, .F. ) ;
#2045=( GEOMETRIC_REPRESENTATION_CONTEXT ( 3 ) GLOBAL_UNCERTAINTY_ASSIGNED_CONTEXT ( ( #897 ) ) GLOBAL_UNIT_ASSIGNED_CONTEXT ( ( #10067, #6256, #11111 ) ) REPRESENTATION_CONTEXT ( 'NONE', 'WORKASPACE' ) );
#2055=DIRECTION ( 'NONE',  ( 0.000000000000000000, 0.000000000000000000, 1.000000000000000000 ) ) ;
#2057=ORIENTED_EDGE ( 'NONE', *, *, #2972, .F. ) ;
#2060=DIRECTION ( 'NONE',  ( -1.000000000000000000, 0.000000000000000000, 0.000000000000000000 ) ) ;
#2076=VERTEX_POINT ( 'NONE', #1260 ) ;
#2086=ORIENTED_EDGE ( 'NONE', *, *, #1023, .F. ) ;
#2090=EDGE_CURVE ( 'NONE', #10859, #3765, #134, .T. ) ;
#2093=CARTESIAN_POINT ( 'NONE',  ( 4.999999999999999112, 5.622796541391564595, 13.09267581720868989 ) ) ;
#2094=DIRECTION ( 'NONE',  ( -1.000000000000000000, 0.000000000000000000, 0.000000000000000000 ) ) ;
#2095=ORIENTED_EDGE ( 'NONE', *, *, #3826, .F. ) ;
#2105=CARTESIAN_POINT ( 'NONE',  ( 4.999999999999999112, -15.22291137398932470, 14.46592441914959082 ) ) ;
#2107=CARTESIAN_POINT ( 'NONE',  ( 0.000000000000000000, 0.000000000000000000, 0.000000000000000000 ) ) ;
#2113=DIRECTION ( 'NONE',  ( 0.000000000000000000, 0.000000000000000000, 1.000000000000000000 ) ) ;
#2115=CARTESIAN_POINT ( 'NONE',  ( 4.999999999999999112, -14.40062958310471686, 8.872489362018137982 ) ) ;
#2116=EDGE_CURVE ( 'NONE', #11746, #12042, #1133, .T. ) ;
#2135=ORIENTED_EDGE ( 'NONE', *, *, #3047, .F. ) ;
#2136=DIRECTION ( 'NONE',  ( 1.000000000000000000, 0.000000000000000000, 0.000000000000000000 ) ) ;
#2151=VERTEX_POINT ( 'NONE', #5073 ) ;
#2152=CARTESIAN_POINT ( 'NONE',  ( 4.999999999999999112, 0.000000000000000000, 0.000000000000000000 ) ) ;
#2164=CARTESIAN_POINT ( 'NONE',  ( 4.999999999999999112, -14.40062958310459251, -1.672489362011137404 ) ) ;
#2165=AXIS2_PLACEMENT_3D ( 'NONE', #9508, #178, #4745 ) ;
#2169=DIRECTION ( 'NONE',  ( 0.000000000000000000, -0.5000000000000071054, 0.8660254037844345998 ) ) ;
#2170=AXIS2_PLACEMENT_3D ( 'NONE', #6400, #9341, #5469 ) ;
#2172=VECTOR ( 'NONE', #862, 1000.000000000000000 ) ;
#2174=ORIENTED_EDGE ( 'NONE', *, *, #4924, .F. ) ;
#2175=CARTESIAN_POINT ( 'NONE',  ( 4.999999999999999112, -14.40062958310459251, -8.872489362018340486 ) ) ;
#2177=VERTEX_POINT ( 'NONE', #10999 ) ;
#2183=EDGE_CURVE ( 'NONE', #2572, #866, #5187, .T. ) ;
#2189=CIRCLE ( 'NONE', #7187, 21.00000000002100009 ) ;
#2193=CARTESIAN_POINT ( 'NONE',  ( 0.000000000000000000, 20.13931372320397273, -5.950465759858654557 ) ) ;
#2195=ORIENTED_EDGE ( 'NONE', *, *, #10853, .F. ) ;
#2196=DIRECTION ( 'NONE',  ( -1.000000000000000000, 0.000000000000000000, 0.000000000000000000 ) ) ;
#2197=CARTESIAN_POINT ( 'NONE',  ( 4.999999999999999112, -5.950465759859008941, 20.13931372320386259 ) ) ;
#2207=EDGE_CURVE ( 'NONE', #2502, #542, #9204, .T. ) ;
#2208=EDGE_CURVE ( 'NONE', #8328, #3785, #5317, .T. ) ;
#2226=LINE ( 'NONE', #8117, #10619 ) ;
#2234=CYLINDRICAL_SURFACE ( 'NONE', #228, 7.200000000007202416 ) ;
#2239=ADVANCED_FACE ( 'NONE', ( #4679 ), #5261, .T. ) ;
#2242=AXIS2_PLACEMENT_3D ( 'NONE', #11504, #7717, #1897 ) ;
#2248=CARTESIAN_POINT ( 'NONE',  ( 0.000000000000000000, -16.90755573046745752, 6.716513609244448624 ) ) ;
#2250=DIRECTION ( 'NONE',  ( -1.000000000000000000, 0.000000000000000000, 0.000000000000000000 ) ) ;
#2251=CARTESIAN_POINT ( 'NONE',  ( 4.999999999999999112, -8.035066368449308882, 14.88411597386726193 ) ) ;
#2259=DIRECTION ( 'NONE',  ( -1.000000000000000000, -0.000000000000000000, 0.000000000000000000 ) ) ;
#2275=LINE ( 'NONE', #385, #10551 ) ;
#2279=ORIENTED_EDGE ( 'NONE', *, *, #3566, .T. ) ;
#2283=EDGE_CURVE ( 'NONE', #12241, #1609, #11379, .T. ) ;
#2284=EDGE_CURVE ( 'NONE', #6613, #26, #5406, .T. ) ;
#2286=DIRECTION ( 'NONE',  ( -1.000000000000000000, -0.000000000000000000, -0.000000000000000000 ) ) ;
#2287=DIRECTION ( 'NONE',  ( -1.000000000000000000, 0.000000000000000000, 0.000000000000000000 ) ) ;
#2290=CYLINDRICAL_SURFACE ( 'NONE', #5213, 14.24900000001425227 ) ;
#2291=ORIENTED_EDGE ( 'NONE', *, *, #6309, .F. ) ;
#2296=DIRECTION ( 'NONE',  ( -1.000000000000000000, 0.000000000000000000, 0.000000000000000000 ) ) ;
#2309=DIRECTION ( 'NONE',  ( -1.000000000000000000, -0.000000000000000000, -0.000000000000000000 ) ) ;
#2312=FACE_OUTER_BOUND ( 'NONE', #2862, .T. ) ;
#2322=DIRECTION ( 'NONE',  ( -1.000000000000000000, -0.000000000000000000, -0.000000000000000000 ) ) ;
#2337=CARTESIAN_POINT ( 'NONE',  ( 4.999999999999997335, 0.000000000000000000, 0.000000000000000000 ) ) ;
#2338=CARTESIAN_POINT ( 'NONE',  ( 4.999999999999999112, 8.527191590521233877, -11.41582255376064126 ) ) ;
#2340=DIRECTION ( 'NONE',  ( -1.000000000000000000, 0.000000000000000000, 0.000000000000000000 ) ) ;
#2343=ADVANCED_FACE ( 'NONE', ( #9619 ), #10485, .T. ) ;
#2352=ORIENTED_EDGE ( 'NONE', *, *, #5484, .F. ) ;
#2353=EDGE_CURVE ( 'NONE', #5917, #10787, #6630, .T. ) ;
#2360=CARTESIAN_POINT ( 'NONE',  ( 4.999999999999999112, 0.000000000000000000, 14.24900000001425227 ) ) ;
#2364=CIRCLE ( 'NONE', #2165, 7.200000000007202416 ) ;
#2374=CIRCLE ( 'NONE', #6382, 14.24900000001425227 ) ;
#2379=ORIENTED_EDGE ( 'NONE', *, *, #6701, .T. ) ;
#2380=LINE ( 'NONE', #3154, #9429 ) ;
#2382=ADVANCED_FACE ( 'NONE', ( #4976 ), #230, .T. ) ;
#2387=EDGE_CURVE ( 'NONE', #9031, #31, #5616, .T. ) ;
#2402=EDGE_CURVE ( 'NONE', #1109, #7442, #5678, .T. ) ;
#2412=EDGE_LOOP ( 'NONE', ( #5592, #9422, #3936, #5147 ) ) ;
#2421=DIRECTION ( 'NONE',  ( -1.000000000000000000, -0.000000000000000000, 0.000000000000000000 ) ) ;
#2430=ORIENTED_EDGE ( 'NONE', *, *, #2884, .T. ) ;
#2439=CARTESIAN_POINT ( 'NONE',  ( 4.999999999999997335, 0.000000000000000000, 0.000000000000000000 ) ) ;
#2448=ORIENTED_EDGE ( 'NONE', *, *, #11359, .F. ) ;
#2460=EDGE_LOOP ( 'NONE', ( #11520, #8365, #3341, #7305 ) ) ;
#2464=DIRECTION ( 'NONE',  ( 0.000000000000000000, 0.000000000000000000, -1.000000000000000000 ) ) ;
#2475=CARTESIAN_POINT ( 'NONE',  ( 2.499999999999998668, -14.46592441914954286, -15.22291137398937089 ) ) ;
#2477=ADVANCED_FACE ( 'NONE', ( #3170 ), #6980, .T. ) ;
#2481=ADVANCED_FACE ( 'NONE', ( #4156 ), #2290, .T. ) ;
#2485=DIRECTION ( 'NONE',  ( 0.000000000000000000, 0.8660254037844363761, 0.5000000000000041078 ) ) ;
#2487=DIRECTION ( 'NONE',  ( -1.000000000000000000, 0.000000000000000000, -0.000000000000000000 ) ) ;
#2493=EDGE_CURVE ( 'NONE', #5118, #2913, #227, .T. ) ;
#2498=CIRCLE ( 'NONE', #11680, 7.200000000007200640 ) ;
#2502=VERTEX_POINT ( 'NONE', #8878 ) ;
#2503=EDGE_LOOP ( 'NONE', ( #1450, #8286, #2352, #8726 ) ) ;
#2507=ORIENTED_EDGE ( 'NONE', *, *, #9297, .T. ) ;
#2509=ORIENTED_EDGE ( 'NONE', *, *, #2353, .F. ) ;
#2510=DIRECTION ( 'NONE',  ( -1.000000000000000000, 0.000000000000000000, -0.000000000000000000 ) ) ;
#2516=CYLINDRICAL_SURFACE ( 'NONE', #5772, 7.200000000007204193 ) ;
#2519=ORIENTED_EDGE ( 'NONE', *, *, #7762, .T. ) ;
#2526=DIRECTION ( 'NONE',  ( 0.000000000000000000, 1.000000000000000000, 3.491481338843133355E-15 ) ) ;
#2529=DIRECTION ( 'NONE',  ( 0.000000000000000000, 0.000000000000000000, 1.000000000000000000 ) ) ;
#2532=VERTEX_POINT ( 'NONE', #9117 ) ;
#2534=FACE_OUTER_BOUND ( 'NONE', #9884, .T. ) ;
#2538=EDGE_CURVE ( 'NONE', #9354, #5416, #4620, .T. ) ;
#2540=DIRECTION ( 'NONE',  ( -1.000000000000000000, 0.000000000000000000, 0.000000000000000000 ) ) ;
#2550=CYLINDRICAL_SURFACE ( 'NONE', #3972, 21.00000000002100009 ) ;
#2554=ORIENTED_EDGE ( 'NONE', *, *, #1821, .T. ) ;
#2563=AXIS2_PLACEMENT_3D ( 'NONE', #2175, #7817, #7940 ) ;
#2569=AXIS2_PLACEMENT_3D ( 'NONE', #7427, #6543, #10343 ) ;
#2571=CIRCLE ( 'NONE', #2771, 14.24900000001425227 ) ;
#2572=VERTEX_POINT ( 'NONE', #4107 ) ;
#2573=CARTESIAN_POINT ( 'NONE',  ( 4.999999999999999112, 14.40062958310465469, -8.872489362018239234 ) ) ;
#2583=EDGE_CURVE ( 'NONE', #3460, #12042, #1616, .T. ) ;
#2585=LINE ( 'NONE', #7350, #2992 ) ;
#2587=FACE_OUTER_BOUND ( 'NONE', #3038, .T. ) ;
#2606=( NAMED_UNIT ( * ) PLANE_ANGLE_UNIT ( ) SI_UNIT ( $, .RADIAN. ) );
#2616=CIRCLE ( 'NONE', #24, 21.00000000002100009 ) ;
#2621=CARTESIAN_POINT ( 'NONE',  ( 0.000000000000000000, -0.4834863907624570856, -16.90755573046746463 ) ) ;
#2624=DIRECTION ( 'NONE',  ( 0.000000000000000000, 0.000000000000000000, 1.000000000000000000 ) ) ;
#2635=AXIS2_PLACEMENT_3D ( 'NONE', #8902, #1262, #5076 ) ;
#2637=CARTESIAN_POINT ( 'NONE',  ( 4.999999999999999112, -13.09267581720870766, 5.622796541391519298 ) ) ;
#2648=LINE ( 'NONE', #11270, #475 ) ;
#2657=CYLINDRICAL_SURFACE ( 'NONE', #4381, 14.24900000001425227 ) ;
#2658=CARTESIAN_POINT ( 'NONE',  ( 4.999999999999999112, 13.09267581720874674, -5.622796541391427816 ) ) ;
#2665=CARTESIAN_POINT ( 'NONE',  ( 4.999999999999999112, -1.676853263447787068, -14.14998813191271410 ) ) ;
#2686=DIRECTION ( 'NONE',  ( -1.000000000000000000, -0.000000000000000000, -0.000000000000000000 ) ) ;
#2687=CARTESIAN_POINT ( 'NONE',  ( 4.999999999999999112, 11.41582255376072830, 8.527191590521114861 ) ) ;
#2689=ORIENTED_EDGE ( 'NONE', *, *, #3428, .F. ) ;
#2690=CARTESIAN_POINT ( 'NONE',  ( 4.999999999999999112, 0.4834863907628118573, -16.90755573046745397 ) ) ;
#2709=LINE ( 'NONE', #5713, #1600 ) ;
#2713=CARTESIAN_POINT ( 'NONE',  ( -10.00000000000000000, 0.000000000000000000, 0.000000000000000000 ) ) ;
#2716=ORIENTED_EDGE ( 'NONE', *, *, #2718, .T. ) ;
#2718=EDGE_CURVE ( 'NONE', #5984, #2502, #5590, .T. ) ;
#2728=ORIENTED_EDGE ( 'NONE', *, *, #2183, .T. ) ;
#2732=CARTESIAN_POINT ( 'NONE',  ( 4.999999999999999112, -11.41582255376066968, -8.527191590521194797 ) ) ;
#2735=PLANE ( 'NONE',  #3030 ) ;
#2744=ORIENTED_EDGE ( 'NONE', *, *, #8460, .F. ) ;
#2753=ORIENTED_EDGE ( 'NONE', *, *, #6389, .T. ) ;
#2759=AXIS2_PLACEMENT_3D ( 'NONE', #11486, #3688, #1741 ) ;
#2771=AXIS2_PLACEMENT_3D ( 'NONE', #541, #9317, #9188 ) ;
#2772=CARTESIAN_POINT ( 'NONE',  ( 0.000000000000000000, -13.09267581720870766, 5.622796541391519298 ) ) ;
#2794=VERTEX_POINT ( 'NONE', #3849 ) ;
#2796=VERTEX_POINT ( 'NONE', #3034 ) ;
#2802=AXIS2_PLACEMENT_3D ( 'NONE', #5540, #7608, #10290 ) ;
#2808=ORIENTED_EDGE ( 'NONE', *, *, #547, .T. ) ;
#2809=ORIENTED_EDGE ( 'NONE', *, *, #3047, .T. ) ;
#2812=AXIS2_PLACEMENT_3D ( 'NONE', #2439, #6193, #618 ) ;
#2815=DIRECTION ( 'NONE',  ( -1.000000000000000000, -0.000000000000000000, -0.000000000000000000 ) ) ;
#2817=ORIENTED_EDGE ( 'NONE', *, *, #74, .F. ) ;
#2824=AXIS2_PLACEMENT_3D ( 'NONE', #1555, #5376, #1050 ) ;
#2857=AXIS2_PLACEMENT_3D ( 'NONE', #9654, #9468, #1081 ) ;
#2859=AXIS2_PLACEMENT_3D ( 'NONE', #6449, #10250, #740 ) ;
#2862=EDGE_LOOP ( 'NONE', ( #2554, #9744, #4768, #5323 ) ) ;
#2872=ADVANCED_FACE ( 'NONE', ( #7729 ), #5855, .T. ) ;
#2876=ORIENTED_EDGE ( 'NONE', *, *, #7490, .F. ) ;
#2879=EDGE_CURVE ( 'NONE', #1723, #2076, #10212, .T. ) ;
#2884=EDGE_CURVE ( 'NONE', #10051, #7451, #8597, .T. ) ;
#2885=VECTOR ( 'NONE', #9967, 1000.000000000000000 ) ;
#2891=ORIENTED_EDGE ( 'NONE', *, *, #3710, .T. ) ;
#2903=CARTESIAN_POINT ( 'NONE',  ( 2.499999999999999556, -20.41639017900856246, -4.916402349214798129 ) ) ;
#2904=AXIS2_PLACEMENT_3D ( 'NONE', #7004, #6070, #6004 ) ;
#2910=EDGE_CURVE ( 'NONE', #9806, #7902, #619, .T. ) ;
#2912=DIRECTION ( 'NONE',  ( 0.000000000000000000, 0.000000000000000000, 1.000000000000000000 ) ) ;
#2913=VERTEX_POINT ( 'NONE', #11397 ) ;
#2916=ORIENTED_EDGE ( 'NONE', *, *, #11833, .F. ) ;
#2931=ORIENTED_EDGE ( 'NONE', *, *, #5478, .T. ) ;
#2954=ORIENTED_EDGE ( 'NONE', *, *, #2402, .T. ) ;
#2956=ORIENTED_EDGE ( 'NONE', *, *, #7064, .F. ) ;
#2959=DIRECTION ( 'NONE',  ( 0.000000000000000000, -6.987080667121815555E-15, 1.000000000000000000 ) ) ;
#2972=EDGE_CURVE ( 'NONE', #7442, #3694, #11801, .T. ) ;
#2974=AXIS2_PLACEMENT_3D ( 'NONE', #11545, #2997, #11363 ) ;
#2983=AXIS2_PLACEMENT_3D ( 'NONE', #9772, #2196, #139 ) ;
#2992=VECTOR ( 'NONE', #6410, 1000.000000000000000 ) ;
#2997=DIRECTION ( 'NONE',  ( -1.000000000000000000, -0.000000000000000000, -0.000000000000000000 ) ) ;
#3000=FACE_OUTER_BOUND ( 'NONE', #8809, .T. ) ;
#3010=DIRECTION ( 'NONE',  ( 0.000000000000000000, -0.4999999999999888978, -0.8660254037844450359 ) ) ;
#3013=AXIS2_PLACEMENT_3D ( 'NONE', #8253, #5546, #6432 ) ;
#3018=CARTESIAN_POINT ( 'NONE',  ( 4.999999999999999112, 8.872489362018189496, 14.40062958310468666 ) ) ;
#3020=EDGE_LOOP ( 'NONE', ( #3175, #3631, #12291, #5387, #9567, #11463, #3509, #3744, #10426, #11532, #8712, #1056, #10101, #2507, #5882, #1426, #8110, #11225, #11995, #2931, #11909, #3108, #2809, #8828, #12335, #4566, #5162, #4206, #2956, #7908, #3917, #11874, #10952, #3919, #4515, #5928, #11365, #2174, #8575, #450, #1178, #7054, #7931, #3988, #11877, #223, #34, #7861, #5977, #9792, #9004, #2448, #407 ) ) ;
#3025=ADVANCED_FACE ( 'NONE', ( #6037 ), #461, .T. ) ;
#3030=AXIS2_PLACEMENT_3D ( 'NONE', #6554, #10360, #1802 ) ;
#3032=CARTESIAN_POINT ( 'NONE',  ( 0.000000000000000000, 6.799999999999999822, 0.000000000000000000 ) ) ;
#3034=CARTESIAN_POINT ( 'NONE',  ( 0.000000000000000000, -4.916402349214727963, 20.41639017900857667 ) ) ;
#3038=EDGE_LOOP ( 'NONE', ( #9678, #1829, #152, #55 ) ) ;
#3041=VECTOR ( 'NONE', #2510, 1000.000000000000000 ) ;
#3043=EDGE_CURVE ( 'NONE', #8435, #8560, #9036, .T. ) ;
#3047=EDGE_CURVE ( 'NONE', #4839, #8928, #8849, .T. ) ;
#3055=DIRECTION ( 'NONE',  ( -1.000000000000000000, -0.000000000000000000, 0.000000000000000000 ) ) ;
#3064=VECTOR ( 'NONE', #6298, 1000.000000000000000 ) ;
#3069=ORIENTED_EDGE ( 'NONE', *, *, #11678, .F. ) ;
#3082=DIRECTION ( 'NONE',  ( -1.000000000000000000, 0.000000000000000000, -0.000000000000000000 ) ) ;
#3084=VERTEX_POINT ( 'NONE', #4326 ) ;
#3096=ORIENTED_EDGE ( 'NONE', *, *, #4781, .F. ) ;
#3105=ORIENTED_EDGE ( 'NONE', *, *, #8754, .T. ) ;
#3108=ORIENTED_EDGE ( 'NONE', *, *, #10738, .T. ) ;
#3111=ORIENTED_EDGE ( 'NONE', *, *, #449, .F. ) ;
#3122=ORIENTED_EDGE ( 'NONE', *, *, #1821, .F. ) ;
#3140=DIRECTION ( 'NONE',  ( 0.000000000000000000, 0.000000000000000000, 1.000000000000000000 ) ) ;
#3141=EDGE_CURVE ( 'NONE', #9748, #114, #8250, .T. ) ;
#3143=CARTESIAN_POINT ( 'NONE',  ( 4.999999999999999112, 0.000000000000000000, 0.000000000000000000 ) ) ;
#3146=LINE ( 'NONE', #4255, #1058 ) ;
#3148=DIRECTION ( 'NONE',  ( 0.000000000000000000, 0.000000000000000000, -1.000000000000000000 ) ) ;
#3149=DIRECTION ( 'NONE',  ( -1.000000000000000000, 0.000000000000000000, -0.000000000000000000 ) ) ;
#3150=ORIENTED_EDGE ( 'NONE', *, *, #7887, .F. ) ;
#3154=CARTESIAN_POINT ( 'NONE',  ( 50.00005079999999680, 6.799999999999999822, 1.500000000000000000 ) ) ;
#3159=ORIENTED_EDGE ( 'NONE', *, *, #5852, .F. ) ;
#3164=DIRECTION ( 'NONE',  ( -1.000000000000000000, -0.000000000000000000, -0.000000000000000000 ) ) ;
#3168=CIRCLE ( 'NONE', #5156, 14.24900000001425049 ) ;
#3170=FACE_OUTER_BOUND ( 'NONE', #9688, .T. ) ;
#3171=ORIENTED_EDGE ( 'NONE', *, *, #1570, .F. ) ;
#3172=ORIENTED_EDGE ( 'NONE', *, *, #1649, .T. ) ;
#3175=ORIENTED_EDGE ( 'NONE', *, *, #9835, .T. ) ;
#3195=EDGE_CURVE ( 'NONE', #9779, #5745, #641, .T. ) ;
#3196=AXIS2_PLACEMENT_3D ( 'NONE', #1013, #4706, #8471 ) ;
#3197=CIRCLE ( 'NONE', #7990, 14.24900000001425404 ) ;
#3203=VECTOR ( 'NONE', #10398, 1000.000000000000000 ) ;
#3219=DIRECTION ( 'NONE',  ( -1.000000000000000000, -0.000000000000000000, 0.000000000000000000 ) ) ;
#3220=DIRECTION ( 'NONE',  ( 0.000000000000000000, -0.8660254037844432595, 0.4999999999999920619 ) ) ;
#3227=APPLICATION_CONTEXT ( 'automotive_design' ) ;
#3233=LINE ( 'NONE', #10784, #10005 ) ;
#3236=DIRECTION ( 'NONE',  ( -1.000000000000000000, -0.000000000000000000, 0.000000000000000000 ) ) ;
#3242=STYLED_ITEM ( 'NONE', ( #10987 ), #6615 ) ;
#3244=DIRECTION ( 'NONE',  ( -1.000000000000000000, -0.000000000000000000, -0.000000000000000000 ) ) ;
#3248=LINE ( 'NONE', #7993, #12129 ) ;
#3251=PRODUCT_DEFINITION_FORMATION_WITH_SPECIFIED_SOURCE ( 'ANY', '', #6836, .NOT_KNOWN. ) ;
#3256=AXIS2_PLACEMENT_3D ( 'NONE', #4077, #9716, #5189 ) ;
#3259=CARTESIAN_POINT ( 'NONE',  ( 4.999999999999999112, 8.035066368449411911, -14.88411597386720508 ) ) ;
#3260=CARTESIAN_POINT ( 'NONE',  ( 4.999999999999999112, 0.4834863907628118573, -16.90755573046745397 ) ) ;
#3264=VECTOR ( 'NONE', #4703, 1000.000000000000000 ) ;
#3266=CARTESIAN_POINT ( 'NONE',  ( 50.00005079999999680, 6.799999999999999822, -1.500000000000000000 ) ) ;
#3273=DIRECTION ( 'NONE',  ( 1.000000000000000000, -0.000000000000000000, -0.000000000000000000 ) ) ;
#3280=VERTEX_POINT ( 'NONE', #8469 ) ;
#3283=CARTESIAN_POINT ( 'NONE',  ( 4.999999999999999112, 13.09267581720874674, -5.622796541391427816 ) ) ;
#3289=ORIENTED_EDGE ( 'NONE', *, *, #3043, .F. ) ;
#3304=EDGE_LOOP ( 'NONE', ( #3868, #3993, #10667, #2954 ) ) ;
#3317=EDGE_CURVE ( 'NONE', #10227, #9587, #6046, .T. ) ;
#3319=CARTESIAN_POINT ( 'NONE',  ( 2.499999999999999556, 20.13931372320388391, 5.950465759858938775 ) ) ;
#3321=PLANE ( 'NONE',  #5184 ) ;
#3339=CARTESIAN_POINT ( 'NONE',  ( 4.999999999999999112, -8.035066368449101049, -14.88411597386737562 ) ) ;
#3340=DIRECTION ( 'NONE',  ( -1.000000000000000000, -0.000000000000000000, 0.000000000000000000 ) ) ;
#3341=ORIENTED_EDGE ( 'NONE', *, *, #3710, .F. ) ;
#3357=LINE ( 'NONE', #7250, #9617 ) ;
#3359=VERTEX_POINT ( 'NONE', #5574 ) ;
#3361=VERTEX_POINT ( 'NONE', #9398 ) ;
#3363=AXIS2_PLACEMENT_3D ( 'NONE', #3808, #4743, #4873 ) ;
#3366=FACE_OUTER_BOUND ( 'NONE', #11200, .T. ) ;
#3367=ORIENTED_EDGE ( 'NONE', *, *, #74, .T. ) ;
#3370=CIRCLE ( 'NONE', #9378, 7.200000000007201528 ) ;
#3377=ORIENTED_EDGE ( 'NONE', *, *, #3390, .T. ) ;
#3380=CIRCLE ( 'NONE', #8583, 14.24900000001425227 ) ;
#3381=ORIENTED_EDGE ( 'NONE', *, *, #9150, .F. ) ;
#3389=DIRECTION ( 'NONE',  ( 0.000000000000000000, 0.000000000000000000, 1.000000000000000000 ) ) ;
#3390=EDGE_CURVE ( 'NONE', #10829, #420, #9022, .T. ) ;
#3395=EDGE_CURVE ( 'NONE', #1109, #1723, #11810, .T. ) ;
#3401=VERTEX_POINT ( 'NONE', #8954 ) ;
#3407=DIRECTION ( 'NONE',  ( -1.000000000000000000, 0.000000000000000000, 0.000000000000000000 ) ) ;
#3410=VERTEX_POINT ( 'NONE', #2193 ) ;
#3413=EDGE_CURVE ( 'NONE', #10829, #185, #10631, .T. ) ;
#3415=CIRCLE ( 'NONE', #2016, 14.24900000001425049 ) ;
#3417=VERTEX_POINT ( 'NONE', #7841 ) ;
#3419=ORIENTED_EDGE ( 'NONE', *, *, #4699, .T. ) ;
#3424=AXIS2_PLACEMENT_3D ( 'NONE', #12031, #10106, #1592 ) ;
#3425=CIRCLE ( 'NONE', #5619, 21.00000000002100009 ) ;
#3428=EDGE_CURVE ( 'NONE', #9779, #2502, #3146, .T. ) ;
#3433=VECTOR ( 'NONE', #7088, 1000.000000000000000 ) ;
#3440=AXIS2_PLACEMENT_3D ( 'NONE', #4459, #4385, #1704 ) ;
#3449=LINE ( 'NONE', #4308, #1862 ) ;
#3460=VERTEX_POINT ( 'NONE', #1371 ) ;
#3463=CYLINDRICAL_SURFACE ( 'NONE', #4356, 7.200000000007202416 ) ;
#3469=FACE_OUTER_BOUND ( 'NONE', #6698, .T. ) ;
#3471=ORIENTED_EDGE ( 'NONE', *, *, #1256, .F. ) ;
#3475=ADVANCED_FACE ( 'NONE', ( #2312 ), #6132, .T. ) ;
#3509=ORIENTED_EDGE ( 'NONE', *, *, #11430, .T. ) ;
#3516=ORIENTED_EDGE ( 'NONE', *, *, #63, .F. ) ;
#3522=CARTESIAN_POINT ( 'NONE',  ( 0.000000000000000000, 11.41582255376084909, -8.527191590520953213 ) ) ;
#3546=VERTEX_POINT ( 'NONE', #6953 ) ;
#3548=EDGE_CURVE ( 'NONE', #2796, #10027, #11002, .T. ) ;
#3555=DIRECTION ( 'NONE',  ( -1.000000000000000000, -0.000000000000000000, -0.000000000000000000 ) ) ;
#3556=ORIENTED_EDGE ( 'NONE', *, *, #3390, .F. ) ;
#3557=CARTESIAN_POINT ( 'NONE',  ( 0.000000000000000000, 0.000000000000000000, 0.000000000000000000 ) ) ;
#3560=VECTOR ( 'NONE', #7965, 1000.000000000000000 ) ;
#3565=CYLINDRICAL_SURFACE ( 'NONE', #4857, 14.24900000001425227 ) ;
#3566=EDGE_CURVE ( 'NONE', #11321, #5923, #7048, .T. ) ;
#3567=CARTESIAN_POINT ( 'NONE',  ( 4.999999999999999112, -14.14998813191268390, -1.676853263448035536 ) ) ;
#3584=ORIENTED_EDGE ( 'NONE', *, *, #1554, .F. ) ;
#3593=CIRCLE ( 'NONE', #5586, 21.00000000002100009 ) ;
#3596=EDGE_CURVE ( 'NONE', #11316, #4059, #11824, .T. ) ;
#3610=ORIENTED_EDGE ( 'NONE', *, *, #3623, .T. ) ;
#3618=AXIS2_PLACEMENT_3D ( 'NONE', #10678, #3798, #5734 ) ;
#3623=EDGE_CURVE ( 'NONE', #1333, #7347, #5853, .T. ) ;
#3629=DIRECTION ( 'NONE',  ( 0.000000000000000000, 0.000000000000000000, 1.000000000000000000 ) ) ;
#3630=DIRECTION ( 'NONE',  ( 0.000000000000000000, -6.987080667121817133E-15, 1.000000000000000000 ) ) ;
#3631=ORIENTED_EDGE ( 'NONE', *, *, #9232, .T. ) ;
#3644=EDGE_CURVE ( 'NONE', #9094, #3359, #3449, .T. ) ;
#3651=AXIS2_PLACEMENT_3D ( 'NONE', #9303, #9243, #6537 ) ;
#3653=FACE_OUTER_BOUND ( 'NONE', #11171, .T. ) ;
#3654=VECTOR ( 'NONE', #6508, 1000.000000000000000 ) ;
#3655=CARTESIAN_POINT ( 'NONE',  ( 4.999999999999999112, -8.872489362018088244, -14.40062958310474883 ) ) ;
#3657=LINE ( 'NONE', #11028, #12251 ) ;
#3662=FACE_OUTER_BOUND ( 'NONE', #8499, .T. ) ;
#3677=VERTEX_POINT ( 'NONE', #10556 ) ;
#3682=ORIENTED_EDGE ( 'NONE', *, *, #2718, .F. ) ;
#3685=DIRECTION ( 'NONE',  ( 0.000000000000000000, 0.4999999999999948375, 0.8660254037844415942 ) ) ;
#3688=DIRECTION ( 'NONE',  ( -1.000000000000000000, 0.000000000000000000, -0.000000000000000000 ) ) ;
#3690=VECTOR ( 'NONE', #10561, 1000.000000000000000 ) ;
#3694=VERTEX_POINT ( 'NONE', #932 ) ;
#3697=FACE_OUTER_BOUND ( 'NONE', #5011, .T. ) ;
#3706=ORIENTED_EDGE ( 'NONE', *, *, #3826, .T. ) ;
#3710=EDGE_CURVE ( 'NONE', #9456, #11316, #3884, .T. ) ;
#3713=VERTEX_POINT ( 'NONE', #11364 ) ;
#3719=DIRECTION ( 'NONE',  ( 0.000000000000000000, 0.000000000000000000, 1.000000000000000000 ) ) ;
#3722=CARTESIAN_POINT ( 'NONE',  ( 2.499999999999999556, 20.41639017900859443, -4.916402349214656020 ) ) ;
#3724=ORIENTED_EDGE ( 'NONE', *, *, #11864, .F. ) ;
#3733=VERTEX_POINT ( 'NONE', #996 ) ;
#3735=CARTESIAN_POINT ( 'NONE',  ( 4.999999999999999112, -8.527191590520994069, -11.41582255376081889 ) ) ;
#3741=DIRECTION ( 'NONE',  ( 0.000000000000000000, 0.5000000000000009992, -0.8660254037844381525 ) ) ;
#3744=ORIENTED_EDGE ( 'NONE', *, *, #3141, .F. ) ;
#3751=LINE ( 'NONE', #6511, #7459 ) ;
#3755=ORIENTED_EDGE ( 'NONE', *, *, #7797, .F. ) ;
#3765=VERTEX_POINT ( 'NONE', #11305 ) ;
#3770=AXIS2_PLACEMENT_3D ( 'NONE', #20, #3846, #7672 ) ;
#3778=DIRECTION ( 'NONE',  ( -1.000000000000000000, -0.000000000000000000, 0.000000000000000000 ) ) ;
#3785=VERTEX_POINT ( 'NONE', #5744 ) ;
#3786=AXIS2_PLACEMENT_3D ( 'NONE', #4831, #7470, #10323 ) ;
#3788=CIRCLE ( 'NONE', #7362, 21.00000000002100009 ) ;
#3790=CIRCLE ( 'NONE', #9187, 5.000000000000000000 ) ;
#3792=ORIENTED_EDGE ( 'NONE', *, *, #3395, .T. ) ;
#3798=DIRECTION ( 'NONE',  ( -1.000000000000000000, -0.000000000000000000, 0.000000000000000000 ) ) ;
#3802=CARTESIAN_POINT ( 'NONE',  ( 4.999999999999999112, 1.676853263448085052, -14.14998813191267857 ) ) ;
#3808=CARTESIAN_POINT ( 'NONE',  ( 4.999999999999999112, 14.88411597386740404, -8.035066368449049534 ) ) ;
#3821=CARTESIAN_POINT ( 'NONE',  ( 4.999999999999999112, 0.000000000000000000, 0.000000000000000000 ) ) ;
#3826=EDGE_CURVE ( 'NONE', #629, #5533, #10652, .T. ) ;
#3834=VERTEX_POINT ( 'NONE', #2687 ) ;
#3835=DIRECTION ( 'NONE',  ( 0.000000000000000000, 0.000000000000000000, 1.000000000000000000 ) ) ;
#3836=CARTESIAN_POINT ( 'NONE',  ( 0.000000000000000000, -0.4834863907626938961, 16.90755573046746107 ) ) ;
#3844=AXIS2_PLACEMENT_3D ( 'NONE', #11834, #3219, #10093 ) ;
#3846=DIRECTION ( 'NONE',  ( -1.000000000000000000, -0.000000000000000000, -0.000000000000000000 ) ) ;
#3848=DIRECTION ( 'NONE',  ( -1.000000000000000000, 0.000000000000000000, 0.000000000000000000 ) ) ;
#3849=CARTESIAN_POINT ( 'NONE',  ( 0.000000000000000000, 14.14998813191269633, -1.676853263447935394 ) ) ;
#3860=EDGE_CURVE ( 'NONE', #2532, #5984, #6942, .T. ) ;
#3863=ORIENTED_EDGE ( 'NONE', *, *, #11942, .F. ) ;
#3868=ORIENTED_EDGE ( 'NONE', *, *, #12168, .F. ) ;
#3884=LINE ( 'NONE', #6643, #3654 ) ;
#3886=DIRECTION ( 'NONE',  ( -1.000000000000000000, -0.000000000000000000, -0.000000000000000000 ) ) ;
#3890=CARTESIAN_POINT ( 'NONE',  ( 50.00005079999999680, 6.799999999999999822, 1.500000000000000000 ) ) ;
#3896=CARTESIAN_POINT ( 'NONE',  ( 4.999999999999999112, -4.916402349214724410, 20.41639017900857667 ) ) ;
#3899=CYLINDRICAL_SURFACE ( 'NONE', #7582, 5.000000000000000000 ) ;
#3917=ORIENTED_EDGE ( 'NONE', *, *, #5852, .T. ) ;
#3919=ORIENTED_EDGE ( 'NONE', *, *, #5884, .F. ) ;
#3922=CARTESIAN_POINT ( 'NONE',  ( 4.999999999999999112, -14.14998813191270877, 1.676853263447836584 ) ) ;
#3929=DIRECTION ( 'NONE',  ( 0.000000000000000000, 0.000000000000000000, -1.000000000000000000 ) ) ;
#3936=ORIENTED_EDGE ( 'NONE', *, *, #8151, .T. ) ;
#3937=FACE_OUTER_BOUND ( 'NONE', #7296, .T. ) ;
#3939=ADVANCED_FACE ( 'NONE', ( #11621 ), #5889, .T. ) ;
#3946=CARTESIAN_POINT ( 'NONE',  ( 2.499999999999999556, -20.13931372320393010, 5.950465759858794002 ) ) ;
#3954=CARTESIAN_POINT ( 'NONE',  ( 0.000000000000000000, 5.622796541391748448, -13.09267581720860996 ) ) ;
#3968=VERTEX_POINT ( 'NONE', #6453 ) ;
#3972=AXIS2_PLACEMENT_3D ( 'NONE', #12170, #2686, #3629 ) ;
#3975=EDGE_LOOP ( 'NONE', ( #3724, #4175, #4275, #705 ) ) ;
#3988=ORIENTED_EDGE ( 'NONE', *, *, #4809, .T. ) ;
#3993=ORIENTED_EDGE ( 'NONE', *, *, #2183, .F. ) ;
#4000=EDGE_LOOP ( 'NONE', ( #10451, #3419, #3377, #9501 ) ) ;
#4004=CIRCLE ( 'NONE', #6824, 21.00000000002100009 ) ;
#4008=AXIS2_PLACEMENT_3D ( 'NONE', #7874, #7926, #7051 ) ;
#4016=EDGE_CURVE ( 'NONE', #7902, #10792, #8656, .T. ) ;
#4019=AXIS2_PLACEMENT_3D ( 'NONE', #8497, #7271, #6689 ) ;
#4020=CIRCLE ( 'NONE', #9015, 7.200000000007203305 ) ;
#4030=DIRECTION ( 'NONE',  ( 0.000000000000000000, 0.4999999999999950040, 0.8660254037844414832 ) ) ;
#4035=DIRECTION ( 'NONE',  ( 0.000000000000000000, 0.000000000000000000, 1.000000000000000000 ) ) ;
#4048=CARTESIAN_POINT ( 'NONE',  ( 4.999999999999999112, -8.035066368449308882, 14.88411597386726193 ) ) ;
#4052=ORIENTED_EDGE ( 'NONE', *, *, #9260, .F. ) ;
#4053=CIRCLE ( 'NONE', #6855, 7.200000000007203305 ) ;
#4059=VERTEX_POINT ( 'NONE', #692 ) ;
#4061=CARTESIAN_POINT ( 'NONE',  ( 4.999999999999999112, 4.916402349214584078, 20.41639017900861219 ) ) ;
#4064=CARTESIAN_POINT ( 'NONE',  ( 0.000000000000000000, 14.46592441914965121, 15.22291137398927141 ) ) ;
#4068=DIRECTION ( 'NONE',  ( -1.000000000000000000, -0.000000000000000000, -0.000000000000000000 ) ) ;
#4070=VECTOR ( 'NONE', #774, 1000.000000000000000 ) ;
#4077=CARTESIAN_POINT ( 'NONE',  ( 4.999999999999999112, 0.4834863907625768231, 16.90755573046746463 ) ) ;
#4079=ADVANCED_FACE ( 'NONE', ( #4506 ), #3565, .T. ) ;
#4080=DIRECTION ( 'NONE',  ( -1.000000000000000000, 0.000000000000000000, 0.000000000000000000 ) ) ;
#4081=DIRECTION ( 'NONE',  ( -1.000000000000000000, -0.000000000000000000, -0.000000000000000000 ) ) ;
#4086=DIRECTION ( 'NONE',  ( -1.000000000000000000, 0.000000000000000000, 0.000000000000000000 ) ) ;
#4088=EDGE_CURVE ( 'NONE', #6055, #4490, #8265, .T. ) ;
#4095=EDGE_CURVE ( 'NONE', #1217, #2572, #4458, .T. ) ;
#4099=VERTEX_POINT ( 'NONE', #12242 ) ;
#4107=CARTESIAN_POINT ( 'NONE',  ( 4.999999999999999112, -5.622796541391473113, -13.09267581720872720 ) ) ;
#4109=EDGE_CURVE ( 'NONE', #8590, #9383, #3751, .T. ) ;
#4116=DIRECTION ( 'NONE',  ( -1.000000000000000000, 0.000000000000000000, 0.000000000000000000 ) ) ;
#4120=CARTESIAN_POINT ( 'NONE',  ( 2.499999999999999556, -20.13931372320384128, -5.950465759859079995 ) ) ;
#4125=DIRECTION ( 'NONE',  ( -1.000000000000000000, 0.000000000000000000, 0.000000000000000000 ) ) ;
#4126=ORIENTED_EDGE ( 'NONE', *, *, #7763, .T. ) ;
#4137=ORIENTED_EDGE ( 'NONE', *, *, #3317, .T. ) ;
#4139=ORIENTED_EDGE ( 'NONE', *, *, #6716, .T. ) ;
#4144=ORIENTED_EDGE ( 'NONE', *, *, #4347, .T. ) ;
#4154=CIRCLE ( 'NONE', #1360, 21.00000000002100009 ) ;
#4156=FACE_OUTER_BOUND ( 'NONE', #8799, .T. ) ;
#4168=EDGE_CURVE ( 'NONE', #9094, #8024, #1274, .T. ) ;
#4171=ORIENTED_EDGE ( 'NONE', *, *, #10444, .F. ) ;
#4175=ORIENTED_EDGE ( 'NONE', *, *, #10509, .T. ) ;
#4177=FACE_OUTER_BOUND ( 'NONE', #1560, .T. ) ;
#4183=VECTOR ( 'NONE', #12167, 1000.000000000000000 ) ;
#4190=CARTESIAN_POINT ( 'NONE',  ( 4.999999999999999112, 0.000000000000000000, 0.000000000000000000 ) ) ;
#4192=CIRCLE ( 'NONE', #10789, 7.200000000007202416 ) ;
#4198=AXIS2_PLACEMENT_3D ( 'NONE', #12320, #11459, #11393 ) ;
#4199=AXIS2_PLACEMENT_3D ( 'NONE', #11870, #9086, #5607 ) ;
#4206=ORIENTED_EDGE ( 'NONE', *, *, #9478, .T. ) ;
#4222=DIRECTION ( 'NONE',  ( 1.000000000000000000, 0.000000000000000000, 0.000000000000000000 ) ) ;
#4225=LINE ( 'NONE', #6235, #8055 ) ;
#4227=EDGE_CURVE ( 'NONE', #8435, #5416, #9385, .T. ) ;
#4242=CARTESIAN_POINT ( 'NONE',  ( 2.499999999999998668, -5.950465759858725612, -20.13931372320394786 ) ) ;
#4244=EDGE_CURVE ( 'NONE', #3280, #8750, #8274, .T. ) ;
#4250=AXIS2_PLACEMENT_3D ( 'NONE', #5266, #8143, #10253 ) ;
#4251=CARTESIAN_POINT ( 'NONE',  ( 4.999999999999999112, -14.14998813191268390, -1.676853263448035536 ) ) ;
#4255=CARTESIAN_POINT ( 'NONE',  ( 50.00005079999999680, 4.769696007084728073, 1.500000000000000000 ) ) ;
#4259=AXIS2_PLACEMENT_3D ( 'NONE', #3259, #2004, #10694 ) ;
#4263=PRODUCT_DEFINITION_CONTEXT ( 'detailed design', #3227, 'design' ) ;
#4267=( NAMED_UNIT ( * ) SI_UNIT ( $, .STERADIAN. ) SOLID_ANGLE_UNIT ( ) );
#4268=CARTESIAN_POINT ( 'NONE',  ( 4.999999999999999112, -14.46592441914954286, -15.22291137398937089 ) ) ;
#4272=DIRECTION ( 'NONE',  ( -1.000000000000000000, -0.000000000000000000, -0.000000000000000000 ) ) ;
#4275=ORIENTED_EDGE ( 'NONE', *, *, #11678, .T. ) ;
#4279=CARTESIAN_POINT ( 'NONE',  ( 0.000000000000000000, 20.41639017900859443, 4.916402349214656020 ) ) ;
#4281=CARTESIAN_POINT ( 'NONE',  ( 4.999999999999999112, -13.09267581720863127, -5.622796541391703151 ) ) ;
#4283=CYLINDRICAL_SURFACE ( 'NONE', #235, 21.00000000002100009 ) ;
#4285=ORIENTED_EDGE ( 'NONE', *, *, #6091, .T. ) ;
#4297=CARTESIAN_POINT ( 'NONE',  ( 4.999999999999999112, 8.527191590521233877, -11.41582255376064126 ) ) ;
#4308=CARTESIAN_POINT ( 'NONE',  ( 4.999999999999999112, -11.41582255376079047, 8.527191590521034925 ) ) ;
#4310=ORIENTED_EDGE ( 'NONE', *, *, #4347, .F. ) ;
#4321=ORIENTED_EDGE ( 'NONE', *, *, #3644, .F. ) ;
#4322=ADVANCED_FACE ( 'NONE', ( #3000 ), #11731, .T. ) ;
#4326=CARTESIAN_POINT ( 'NONE',  ( 4.999999999999999112, -14.46592441914974891, 15.22291137398917193 ) ) ;
#4339=CARTESIAN_POINT ( 'NONE',  ( 4.999999999999999112, 0.000000000000000000, 0.000000000000000000 ) ) ;
#4341=VERTEX_POINT ( 'NONE', #721 ) ;
#4345=EDGE_LOOP ( 'NONE', ( #1018, #3584, #10775, #4368 ) ) ;
#4347=EDGE_CURVE ( 'NONE', #185, #4839, #6300, .T. ) ;
#4349=VERTEX_POINT ( 'NONE', #4534 ) ;
#4356=AXIS2_PLACEMENT_3D ( 'NONE', #4456, #8332, #3389 ) ;
#4368=ORIENTED_EDGE ( 'NONE', *, *, #6858, .T. ) ;
#4381=AXIS2_PLACEMENT_3D ( 'NONE', #8412, #5410, #3719 ) ;
#4385=DIRECTION ( 'NONE',  ( -1.000000000000000000, 0.000000000000000000, -0.000000000000000000 ) ) ;
#4389=DIRECTION ( 'NONE',  ( 0.000000000000000000, 0.000000000000000000, 1.000000000000000000 ) ) ;
#4393=UNCERTAINTY_MEASURE_WITH_UNIT (LENGTH_MEASURE( 1.000000000000000082E-05 ), #513, 'distance_accuracy_value', 'NONE');
#4396=EDGE_CURVE ( 'NONE', #2794, #3713, #6269, .T. ) ;
#4397=ORIENTED_EDGE ( 'NONE', *, *, #11406, .F. ) ;
#4398=ADVANCED_FACE ( 'NONE', ( #7488 ), #8244, .T. ) ;
#4404=CYLINDRICAL_SURFACE ( 'NONE', #1429, 14.24900000001425227 ) ;
#4406=VERTEX_POINT ( 'NONE', #11284 ) ;
#4413=ORIENTED_EDGE ( 'NONE', *, *, #1027, .F. ) ;
#4425=DIRECTION ( 'NONE',  ( 0.000000000000000000, 0.000000000000000000, 1.000000000000000000 ) ) ;
#4429=SURFACE_STYLE_USAGE ( .BOTH. , #1612 ) ;
#4436=AXIS2_PLACEMENT_3D ( 'NONE', #3339, #7914, #7966 ) ;
#4437=AXIS2_PLACEMENT_3D ( 'NONE', #3821, #8514, #2055 ) ;
#4440=DIRECTION ( 'NONE',  ( -1.000000000000000000, 0.000000000000000000, -0.000000000000000000 ) ) ;
#4442=DIRECTION ( 'NONE',  ( -1.000000000000000000, 0.000000000000000000, 0.000000000000000000 ) ) ;
#4447=LINE ( 'NONE', #3567, #10621 ) ;
#4456=CARTESIAN_POINT ( 'NONE',  ( 4.999999999999999112, -16.90755573046745752, -0.4834863907627537372 ) ) ;
#4458=CIRCLE ( 'NONE', #11045, 7.200000000007201528 ) ;
#4459=CARTESIAN_POINT ( 'NONE',  ( 0.000000000000000000, 14.88411597386729213, 8.035066368449255592 ) ) ;
#4460=DIRECTION ( 'NONE',  ( 1.000000000000000000, 0.000000000000000000, 0.000000000000000000 ) ) ;
#4467=AXIS2_PLACEMENT_3D ( 'NONE', #2251, #876, #4693 ) ;
#4468=ADVANCED_FACE ( 'NONE', ( #5784 ), #6737, .T. ) ;
#4475=ORIENTED_EDGE ( 'NONE', *, *, #9989, .F. ) ;
#4477=ORIENTED_EDGE ( 'NONE', *, *, #10007, .F. ) ;
#4478=CARTESIAN_POINT ( 'NONE',  ( 4.999999999999999112, 0.000000000000000000, 0.000000000000000000 ) ) ;
#4490=VERTEX_POINT ( 'NONE', #9675 ) ;
#4493=VECTOR ( 'NONE', #4125, 1000.000000000000000 ) ;
#4503=DIRECTION ( 'NONE',  ( 1.000000000000000000, -0.000000000000000000, -0.000000000000000000 ) ) ;
#4506=FACE_OUTER_BOUND ( 'NONE', #9159, .T. ) ;
#4515=ORIENTED_EDGE ( 'NONE', *, *, #10522, .T. ) ;
#4518=ORIENTED_EDGE ( 'NONE', *, *, #3548, .T. ) ;
#4520=CARTESIAN_POINT ( 'NONE',  ( 4.999999999999999112, 0.4834863907625768231, 16.90755573046746463 ) ) ;
#4528=CARTESIAN_POINT ( 'NONE',  ( 4.999999999999999112, 0.000000000000000000, 0.000000000000000000 ) ) ;
#4534=CARTESIAN_POINT ( 'NONE',  ( 0.000000000000000000, -20.13931372320384128, -5.950465759859079995 ) ) ;
#4538=CYLINDRICAL_SURFACE ( 'NONE', #2802, 7.200000000007202416 ) ;
#4556=CIRCLE ( 'NONE', #2759, 7.200000000007202416 ) ;
#4560=ORIENTED_EDGE ( 'NONE', *, *, #2283, .T. ) ;
#4566=ORIENTED_EDGE ( 'NONE', *, *, #12168, .T. ) ;
#4580=EDGE_CURVE ( 'NONE', #3417, #9895, #9793, .T. ) ;
#4584=VERTEX_POINT ( 'NONE', #8920 ) ;
#4586=ORIENTED_EDGE ( 'NONE', *, *, #8092, .F. ) ;
#4597=ORIENTED_EDGE ( 'NONE', *, *, #11230, .F. ) ;
#4617=DIRECTION ( 'NONE',  ( -1.000000000000000000, 0.000000000000000000, 0.000000000000000000 ) ) ;
#4620=CIRCLE ( 'NONE', #7227, 7.200000000007202416 ) ;
#4628=VECTOR ( 'NONE', #6512, 1000.000000000000000 ) ;
#4630=CIRCLE ( 'NONE', #5831, 7.200000000007204193 ) ;
#4646=CARTESIAN_POINT ( 'NONE',  ( 0.000000000000000000, 4.916402349214583190, 20.41639017900861219 ) ) ;
#4651=ORIENTED_EDGE ( 'NONE', *, *, #10946, .T. ) ;
#4652=DIRECTION ( 'NONE',  ( -1.000000000000000000, -0.000000000000000000, -0.000000000000000000 ) ) ;
#4661=EDGE_CURVE ( 'NONE', #5533, #2913, #2648, .T. ) ;
#4665=DIRECTION ( 'NONE',  ( 0.000000000000000000, -1.000000000000000000, 0.000000000000000000 ) ) ;
#4666=ORIENTED_EDGE ( 'NONE', *, *, #4244, .F. ) ;
#4669=ORIENTED_EDGE ( 'NONE', *, *, #4712, .T. ) ;
#4679=FACE_OUTER_BOUND ( 'NONE', #9548, .T. ) ;
#4682=ORIENTED_EDGE ( 'NONE', *, *, #6242, .T. ) ;
#4689=CYLINDRICAL_SURFACE ( 'NONE', #2974, 21.00000000002100009 ) ;
#4691=VERTEX_POINT ( 'NONE', #1766 ) ;
#4693=DIRECTION ( 'NONE',  ( 0.000000000000000000, 0.4999999999999948375, 0.8660254037844415942 ) ) ;
#4699=EDGE_CURVE ( 'NONE', #3546, #10829, #1685, .T. ) ;
#4703=DIRECTION ( 'NONE',  ( -1.000000000000000000, 0.000000000000000000, 0.000000000000000000 ) ) ;
#4706=DIRECTION ( 'NONE',  ( -1.000000000000000000, 0.000000000000000000, 0.000000000000000000 ) ) ;
#4712=EDGE_CURVE ( 'NONE', #866, #3677, #10254, .T. ) ;
#4715=DIRECTION ( 'NONE',  ( -1.000000000000000000, -0.000000000000000000, -0.000000000000000000 ) ) ;
#4716=CARTESIAN_POINT ( 'NONE',  ( 4.999999999999999112, 14.88411597386729213, 8.035066368449255592 ) ) ;
#4725=SHAPE_DEFINITION_REPRESENTATION ( #1131, #1080 ) ;
#4734=DIRECTION ( 'NONE',  ( -1.000000000000000000, -0.000000000000000000, 0.000000000000000000 ) ) ;
#4743=DIRECTION ( 'NONE',  ( -1.000000000000000000, 0.000000000000000000, -0.000000000000000000 ) ) ;
#4745=DIRECTION ( 'NONE',  ( 0.000000000000000000, 1.000000000000000000, 3.373073425507084106E-15 ) ) ;
#4751=DIRECTION ( 'NONE',  ( -1.000000000000000000, -0.000000000000000000, 0.000000000000000000 ) ) ;
#4755=VECTOR ( 'NONE', #6463, 1000.000000000000000 ) ;
#4761=EDGE_CURVE ( 'NONE', #4099, #10051, #6893, .T. ) ;
#4762=DIRECTION ( 'NONE',  ( 1.000000000000000000, 0.000000000000000000, 0.000000000000000000 ) ) ;
#4768=ORIENTED_EDGE ( 'NONE', *, *, #9434, .F. ) ;
#4770=DIRECTION ( 'NONE',  ( 0.000000000000000000, 0.000000000000000000, 1.000000000000000000 ) ) ;
#4781=EDGE_CURVE ( 'NONE', #3968, #4059, #3657, .T. ) ;
#4786=AXIS2_PLACEMENT_3D ( 'NONE', #9950, #2136, #3148 ) ;
#4808=EDGE_CURVE ( 'NONE', #114, #3280, #11, .T. ) ;
#4809=EDGE_CURVE ( 'NONE', #10227, #6613, #292, .T. ) ;
#4816=CARTESIAN_POINT ( 'NONE',  ( 4.999999999999999112, -14.40062958310459251, -1.672489362011137404 ) ) ;
#4831=CARTESIAN_POINT ( 'NONE',  ( 4.999999999999999112, 0.000000000000000000, 0.000000000000000000 ) ) ;
#4832=DIRECTION ( 'NONE',  ( -1.000000000000000000, -0.000000000000000000, 0.000000000000000000 ) ) ;
#4835=ORIENTED_EDGE ( 'NONE', *, *, #4808, .F. ) ;
#4839=VERTEX_POINT ( 'NONE', #9405 ) ;
#4844=FACE_OUTER_BOUND ( 'NONE', #5735, .T. ) ;
#4857=AXIS2_PLACEMENT_3D ( 'NONE', #7387, #11182, #2624 ) ;
#4858=EDGE_CURVE ( 'NONE', #4914, #11321, #896, .T. ) ;
#4863=CARTESIAN_POINT ( 'NONE',  ( 50.00005079999999680, 0.000000000000000000, 1.500000000000000000 ) ) ;
#4870=EDGE_LOOP ( 'NONE', ( #11730, #4923, #272, #7599 ) ) ;
#4871=DIRECTION ( 'NONE',  ( -1.000000000000000000, 0.000000000000000000, -0.000000000000000000 ) ) ;
#4872=ORIENTED_EDGE ( 'NONE', *, *, #1649, .F. ) ;
#4873=DIRECTION ( 'NONE',  ( 0.000000000000000000, 0.000000000000000000, 1.000000000000000000 ) ) ;
#4889=VECTOR ( 'NONE', #11322, 1000.000000000000000 ) ;
#4894=ORIENTED_EDGE ( 'NONE', *, *, #3566, .F. ) ;
#4909=CARTESIAN_POINT ( 'NONE',  ( -10.00000000000000000, 0.000000000000000000, 0.000000000000000000 ) ) ;
#4914=VERTEX_POINT ( 'NONE', #10655 ) ;
#4919=DIRECTION ( 'NONE',  ( -1.000000000000000000, -0.000000000000000000, -0.000000000000000000 ) ) ;
#4921=ORIENTED_EDGE ( 'NONE', *, *, #7592, .F. ) ;
#4923=ORIENTED_EDGE ( 'NONE', *, *, #9584, .F. ) ;
#4924=EDGE_CURVE ( 'NONE', #5416, #11746, #5493, .T. ) ;
#4929=DIRECTION ( 'NONE',  ( 0.000000000000000000, 1.000000000000000000, 0.000000000000000000 ) ) ;
#4931=ORIENTED_EDGE ( 'NONE', *, *, #10613, .T. ) ;
#4959=DIRECTION ( 'NONE',  ( 0.000000000000000000, 0.000000000000000000, 1.000000000000000000 ) ) ;
#4962=EDGE_LOOP ( 'NONE', ( #10356, #4586, #3122, #2808 ) ) ;
#4976=FACE_OUTER_BOUND ( 'NONE', #332, .T. ) ;
#4979=ORIENTED_EDGE ( 'NONE', *, *, #5424, .T. ) ;
#4980=AXIS2_PLACEMENT_3D ( 'NONE', #3557, #7324, #6442 ) ;
#4985=DIRECTION ( 'NONE',  ( -1.000000000000000000, 0.000000000000000000, 0.000000000000000000 ) ) ;
#4995=DIRECTION ( 'NONE',  ( 0.000000000000000000, 0.000000000000000000, 1.000000000000000000 ) ) ;
#4997=CARTESIAN_POINT ( 'NONE',  ( 2.499999999999999556, 15.22291137398942418, -14.46592441914948779 ) ) ;
#5008=CIRCLE ( 'NONE', #6418, 7.200000000007201528 ) ;
#5010=CARTESIAN_POINT ( 'NONE',  ( 4.999999999999999112, 0.000000000000000000, 0.000000000000000000 ) ) ;
#5011=EDGE_LOOP ( 'NONE', ( #5534, #6800, #10442, #1956 ) ) ;
#5013=CARTESIAN_POINT ( 'NONE',  ( 0.000000000000000000, 0.000000000000000000, 0.000000000000000000 ) ) ;
#5017=LINE ( 'NONE', #3283, #9037 ) ;
#5021=CIRCLE ( 'NONE', #10407, 7.200000000007204193 ) ;
#5023=LINE ( 'NONE', #1324, #7200 ) ;
#5046=FACE_OUTER_BOUND ( 'NONE', #1474, .T. ) ;
#5053=AXIS2_PLACEMENT_3D ( 'NONE', #4909, #11580, #6735 ) ;
#5067=CARTESIAN_POINT ( 'NONE',  ( 4.999999999999999112, 1.676853263447885878, 14.14998813191270166 ) ) ;
#5073=CARTESIAN_POINT ( 'NONE',  ( 0.000000000000000000, 1.676853263447885878, 14.14998813191270166 ) ) ;
#5076=DIRECTION ( 'NONE',  ( 0.000000000000000000, -0.8660254037844432595, 0.4999999999999920619 ) ) ;
#5079=DIRECTION ( 'NONE',  ( -1.000000000000000000, -0.000000000000000000, -0.000000000000000000 ) ) ;
#5088=LINE ( 'NONE', #1386, #3560 ) ;
#5104=FACE_OUTER_BOUND ( 'NONE', #801, .T. ) ;
#5105=DIRECTION ( 'NONE',  ( 0.000000000000000000, 1.000000000000000000, 3.491481338843133355E-15 ) ) ;
#5111=DIRECTION ( 'NONE',  ( -1.000000000000000000, 0.000000000000000000, 0.000000000000000000 ) ) ;
#5116=LINE ( 'NONE', #4120, #7969 ) ;
#5118=VERTEX_POINT ( 'NONE', #5273 ) ;
#5132=DIRECTION ( 'NONE',  ( -1.000000000000000000, 0.000000000000000000, 0.000000000000000000 ) ) ;
#5143=FACE_OUTER_BOUND ( 'NONE', #7790, .T. ) ;
#5147=ORIENTED_EDGE ( 'NONE', *, *, #7689, .T. ) ;
#5148=CARTESIAN_POINT ( 'NONE',  ( 2.499999999999999556, 15.22291137398922167, 14.46592441914969918 ) ) ;
#5156=AXIS2_PLACEMENT_3D ( 'NONE', #8859, #8786, #8040 ) ;
#5162=ORIENTED_EDGE ( 'NONE', *, *, #2972, .T. ) ;
#5164=ORIENTED_EDGE ( 'NONE', *, *, #4168, .F. ) ;
#5180=CARTESIAN_POINT ( 'NONE',  ( 0.000000000000000000, 8.872489362018390224, -14.40062958310456054 ) ) ;
#5184=AXIS2_PLACEMENT_3D ( 'NONE', #3266, #438, #7077 ) ;
#5187=LINE ( 'NONE', #8086, #10990 ) ;
#5189=DIRECTION ( 'NONE',  ( 0.000000000000000000, 0.000000000000000000, 1.000000000000000000 ) ) ;
#5194=CARTESIAN_POINT ( 'NONE',  ( 0.000000000000000000, -20.41639017900862996, 4.916402349214513912 ) ) ;
#5205=DIRECTION ( 'NONE',  ( -1.000000000000000000, 0.000000000000000000, 0.000000000000000000 ) ) ;
#5210=ORIENTED_EDGE ( 'NONE', *, *, #711, .T. ) ;
#5213=AXIS2_PLACEMENT_3D ( 'NONE', #1290, #473, #11899 ) ;
#5218=CARTESIAN_POINT ( 'NONE',  ( 0.000000000000000000, -5.950465759859008053, 20.13931372320386259 ) ) ;
#5226=DIRECTION ( 'NONE',  ( 0.000000000000000000, -0.4999999999999889533, -0.8660254037844451469 ) ) ;
#5228=ORIENTED_EDGE ( 'NONE', *, *, #10824, .T. ) ;
#5237=AXIS2_PLACEMENT_3D ( 'NONE', #3260, #10924, #9824 ) ;
#5239=AXIS2_PLACEMENT_3D ( 'NONE', #5010, #7136, #11692 ) ;
#5254=EDGE_CURVE ( 'NONE', #1609, #8601, #7573, .T. ) ;
#5255=ORIENTED_EDGE ( 'NONE', *, *, #7237, .T. ) ;
#5261=CYLINDRICAL_SURFACE ( 'NONE', #4199, 7.200000000007202416 ) ;
#5266=CARTESIAN_POINT ( 'NONE',  ( 0.000000000000000000, 0.000000000000000000, 0.000000000000000000 ) ) ;
#5273=CARTESIAN_POINT ( 'NONE',  ( 0.000000000000000000, -1.676853263447986242, 14.14998813191269100 ) ) ;
#5277=VERTEX_POINT ( 'NONE', #9388 ) ;
#5283=ADVANCED_FACE ( 'NONE', ( #6710 ), #9570, .T. ) ;
#5317=LINE ( 'NONE', #6618, #5604 ) ;
#5323=ORIENTED_EDGE ( 'NONE', *, *, #11230, .T. ) ;
#5333=FACE_OUTER_BOUND ( 'NONE', #9390, .T. ) ;
#5343=EDGE_CURVE ( 'NONE', #9528, #4099, #9493, .T. ) ;
#5355=ORIENTED_EDGE ( 'NONE', *, *, #7913, .F. ) ;
#5360=DIRECTION ( 'NONE',  ( -1.000000000000000000, 0.000000000000000000, 0.000000000000000000 ) ) ;
#5368=DIRECTION ( 'NONE',  ( -1.000000000000000000, -0.000000000000000000, -0.000000000000000000 ) ) ;
#5376=DIRECTION ( 'NONE',  ( -1.000000000000000000, 0.000000000000000000, 0.000000000000000000 ) ) ;
#5387=ORIENTED_EDGE ( 'NONE', *, *, #1734, .T. ) ;
#5388=DIRECTION ( 'NONE',  ( 0.000000000000000000, 0.000000000000000000, -1.000000000000000000 ) ) ;
#5393=CARTESIAN_POINT ( 'NONE',  ( 4.999999999999999112, 0.000000000000000000, 0.000000000000000000 ) ) ;
#5396=CARTESIAN_POINT ( 'NONE',  ( 0.000000000000000000, -14.40062958310459251, -1.672489362011137404 ) ) ;
#5398=ORIENTED_EDGE ( 'NONE', *, *, #4661, .F. ) ;
#5406=CIRCLE ( 'NONE', #2824, 7.200000000007203305 ) ;
#5410=DIRECTION ( 'NONE',  ( -1.000000000000000000, -0.000000000000000000, 0.000000000000000000 ) ) ;
#5416=VERTEX_POINT ( 'NONE', #2248 ) ;
#5419=AXIS2_PLACEMENT_3D ( 'NONE', #4863, #10674, #11594 ) ;
#5424=EDGE_CURVE ( 'NONE', #6441, #7902, #1127, .T. ) ;
#5426=CYLINDRICAL_SURFACE ( 'NONE', #11749, 14.24900000001425227 ) ;
#5436=SHAPE_REPRESENTATION_RELATIONSHIP ( 'NONE' , 'NONE' ,  #1080, #6615 ) ;
#5440=ORIENTED_EDGE ( 'NONE', *, *, #7706, .F. ) ;
#5441=LINE ( 'NONE', #6259, #6797 ) ;
#5469=DIRECTION ( 'NONE',  ( 0.000000000000000000, 0.8660254037844398178, -0.4999999999999980571 ) ) ;
#5472=DIRECTION ( 'NONE',  ( 1.000000000000000000, 0.000000000000000000, 0.000000000000000000 ) ) ;
#5476=FACE_OUTER_BOUND ( 'NONE', #5982, .T. ) ;
#5478=EDGE_CURVE ( 'NONE', #4059, #3401, #300, .T. ) ;
#5484=EDGE_CURVE ( 'NONE', #11913, #2151, #1249, .T. ) ;
#5493=CIRCLE ( 'NONE', #6485, 7.200000000007202416 ) ;
#5494=ORIENTED_EDGE ( 'NONE', *, *, #4088, .T. ) ;
#5498=CARTESIAN_POINT ( 'NONE',  ( 4.999999999999999112, -16.90755573046745752, -0.4834863907627537372 ) ) ;
#5503=DIRECTION ( 'NONE',  ( 0.000000000000000000, 0.000000000000000000, 1.000000000000000000 ) ) ;
#5504=CARTESIAN_POINT ( 'NONE',  ( 4.999999999999999112, 0.000000000000000000, 0.000000000000000000 ) ) ;
#5506=ADVANCED_FACE ( 'NONE', ( #11170 ), #12049, .T. ) ;
#5508=DIRECTION ( 'NONE',  ( 0.000000000000000000, -0.8660254037844328234, -0.5000000000000099920 ) ) ;
#5512=DIRECTION ( 'NONE',  ( 0.000000000000000000, 0.000000000000000000, 1.000000000000000000 ) ) ;
#5517=EDGE_LOOP ( 'NONE', ( #4285, #10634, #10776, #4137 ) ) ;
#5518=CARTESIAN_POINT ( 'NONE',  ( 4.999999999999999112, -4.916402349214441969, -20.41639017900864772 ) ) ;
#5523=ORIENTED_EDGE ( 'NONE', *, *, #6886, .F. ) ;
#5524=CARTESIAN_POINT ( 'NONE',  ( 4.999999999999999112, 14.40062958310465469, -8.872489362018239234 ) ) ;
#5533=VERTEX_POINT ( 'NONE', #2360 ) ;
#5534=ORIENTED_EDGE ( 'NONE', *, *, #4808, .T. ) ;
#5537=DIRECTION ( 'NONE',  ( -1.000000000000000000, 0.000000000000000000, 0.000000000000000000 ) ) ;
#5538=PRODUCT_CONTEXT ( 'NONE', #901, 'mechanical' ) ;
#5540=CARTESIAN_POINT ( 'NONE',  ( 4.999999999999999112, -8.872489362018288972, 14.40062958310462271 ) ) ;
#5544=EDGE_CURVE ( 'NONE', #3713, #7451, #2498, .T. ) ;
#5546=DIRECTION ( 'NONE',  ( -1.000000000000000000, 0.000000000000000000, 0.000000000000000000 ) ) ;
#5556=CIRCLE ( 'NONE', #1568, 14.24900000001425049 ) ;
#5559=ORIENTED_EDGE ( 'NONE', *, *, #2090, .F. ) ;
#5570=CARTESIAN_POINT ( 'NONE',  ( 4.999999999999997335, 4.769696007084728073, -1.500000000000000000 ) ) ;
#5573=CARTESIAN_POINT ( 'NONE',  ( 0.000000000000000000, 0.000000000000000000, 0.000000000000000000 ) ) ;
#5574=CARTESIAN_POINT ( 'NONE',  ( 0.000000000000000000, -11.41582255376079047, 8.527191590521034925 ) ) ;
#5578=CARTESIAN_POINT ( 'NONE',  ( 50.00005079999999680, 0.000000000000000000, 0.000000000000000000 ) ) ;
#5584=AXIS2_PLACEMENT_3D ( 'NONE', #7050, #2286, #528 ) ;
#5586=AXIS2_PLACEMENT_3D ( 'NONE', #8317, #5620, #8507 ) ;
#5587=DIRECTION ( 'NONE',  ( 0.000000000000000000, 0.000000000000000000, 1.000000000000000000 ) ) ;
#5590=LINE ( 'NONE', #9412, #12199 ) ;
#5592=ORIENTED_EDGE ( 'NONE', *, *, #8367, .T. ) ;
#5604=VECTOR ( 'NONE', #7551, 1000.000000000000000 ) ;
#5607=DIRECTION ( 'NONE',  ( 0.000000000000000000, 0.000000000000000000, 1.000000000000000000 ) ) ;
#5610=CARTESIAN_POINT ( 'NONE',  ( 50.00005079999999680, 6.799999999999999822, -1.500000000000000000 ) ) ;
#5616=CIRCLE ( 'NONE', #8823, 14.24900000001425049 ) ;
#5617=EDGE_LOOP ( 'NONE', ( #773, #3516, #8775, #11892, #3682, #1212 ) ) ;
#5618=DIRECTION ( 'NONE',  ( 1.000000000000000000, 0.000000000000000000, -0.000000000000000000 ) ) ;
#5619=AXIS2_PLACEMENT_3D ( 'NONE', #1165, #3244, #10864 ) ;
#5620=DIRECTION ( 'NONE',  ( -1.000000000000000000, -0.000000000000000000, -0.000000000000000000 ) ) ;
#5637=MECHANICAL_DESIGN_GEOMETRIC_PRESENTATION_REPRESENTATION('',(#3242),#2045);
#5638=AXIS2_PLACEMENT_3D ( 'NONE', #5573, #9397, #823 ) ;
#5643=ADVANCED_FACE ( 'NONE', ( #3366 ), #5739, .T. ) ;
#5647=CIRCLE ( 'NONE', #3440, 7.200000000007201528 ) ;
#5651=VECTOR ( 'NONE', #4503, 1000.000000000000000 ) ;
#5654=CARTESIAN_POINT ( 'NONE',  ( 0.000000000000000000, 0.000000000000000000, 0.000000000000000000 ) ) ;
#5655=UNCERTAINTY_MEASURE_WITH_UNIT (LENGTH_MEASURE( 1.000000000000000082E-05 ), #8131, 'distance_accuracy_value', 'NONE');
#5658=DIRECTION ( 'NONE',  ( 0.000000000000000000, 0.4999999999999948930, 0.8660254037844414832 ) ) ;
#5673=ORIENTED_EDGE ( 'NONE', *, *, #8547, .T. ) ;
#5678=LINE ( 'NONE', #9498, #9615 ) ;
#5704=CYLINDRICAL_SURFACE ( 'NONE', #12076, 7.200000000007202416 ) ;
#5711=DIRECTION ( 'NONE',  ( -1.000000000000000000, 0.000000000000000000, 0.000000000000000000 ) ) ;
#5713=CARTESIAN_POINT ( 'NONE',  ( 4.999999999999999112, 14.14998813191269633, -1.676853263447935394 ) ) ;
#5719=ORIENTED_EDGE ( 'NONE', *, *, #12127, .F. ) ;
#5730=ORIENTED_EDGE ( 'NONE', *, *, #3395, .F. ) ;
#5734=DIRECTION ( 'NONE',  ( 0.000000000000000000, -0.8660254037844328234, -0.5000000000000098810 ) ) ;
#5735=EDGE_LOOP ( 'NONE', ( #2519, #4126, #5494, #4475 ) ) ;
#5739=CYLINDRICAL_SURFACE ( 'NONE', #707, 21.00000000002100009 ) ;
#5740=ORIENTED_EDGE ( 'NONE', *, *, #6921, .F. ) ;
#5742=CARTESIAN_POINT ( 'NONE',  ( 4.999999999999999112, -1.676853263447986242, 14.14998813191269100 ) ) ;
#5744=CARTESIAN_POINT ( 'NONE',  ( 4.999999999999999112, 5.950465759858867720, 20.13931372320390523 ) ) ;
#5745=VERTEX_POINT ( 'NONE', #7628 ) ;
#5756=DIRECTION ( 'NONE',  ( 0.000000000000000000, 0.000000000000000000, 1.000000000000000000 ) ) ;
#5757=LINE ( 'NONE', #80, #3264 ) ;
#5762=DIRECTION ( 'NONE',  ( 0.000000000000000000, 0.000000000000000000, -1.000000000000000000 ) ) ;
#5772=AXIS2_PLACEMENT_3D ( 'NONE', #9221, #7404, #6214 ) ;
#5775=DIRECTION ( 'NONE',  ( -1.000000000000000000, 0.000000000000000000, -0.000000000000000000 ) ) ;
#5776=AXIS2_PLACEMENT_3D ( 'NONE', #11057, #2487, #6311 ) ;
#5784=FACE_OUTER_BOUND ( 'NONE', #8272, .T. ) ;
#5787=EDGE_CURVE ( 'NONE', #3359, #4406, #8825, .T. ) ;
#5788=ORIENTED_EDGE ( 'NONE', *, *, #1883, .T. ) ;
#5789=ADVANCED_FACE ( 'NONE', ( #7503, #11300 ), #2735, .F. ) ;
#5794=ORIENTED_EDGE ( 'NONE', *, *, #10509, .F. ) ;
#5801=ADVANCED_FACE ( 'NONE', ( #299 ), #2234, .T. ) ;
#5802=EDGE_CURVE ( 'NONE', #7451, #3410, #3425, .T. ) ;
#5803=AXIS2_PLACEMENT_3D ( 'NONE', #5504, #1744, #797 ) ;
#5815=CARTESIAN_POINT ( 'NONE',  ( 4.999999999999999112, 0.000000000000000000, 0.000000000000000000 ) ) ;
#5818=AXIS2_PLACEMENT_3D ( 'NONE', #3655, #1708, #12193 ) ;
#5831=AXIS2_PLACEMENT_3D ( 'NONE', #1567, #9278, #5388 ) ;
#5832=CARTESIAN_POINT ( 'NONE',  ( 4.999999999999999112, 14.14998813191269633, 1.676853263447936726 ) ) ;
#5836=ORIENTED_EDGE ( 'NONE', *, *, #804, .F. ) ;
#5837=CYLINDRICAL_SURFACE ( 'NONE', #3196, 7.200000000007202416 ) ;
#5852=EDGE_CURVE ( 'NONE', #8559, #4349, #1624, .T. ) ;
#5853=CIRCLE ( 'NONE', #2859, 14.24900000001425049 ) ;
#5855=CYLINDRICAL_SURFACE ( 'NONE', #10809, 7.200000000007202416 ) ;
#5856=ORIENTED_EDGE ( 'NONE', *, *, #6886, .T. ) ;
#5857=ORIENTED_EDGE ( 'NONE', *, *, #10946, .F. ) ;
#5872=CARTESIAN_POINT ( 'NONE',  ( 2.499999999999998668, -20.41639017900862996, 4.916402349214513912 ) ) ;
#5882=ORIENTED_EDGE ( 'NONE', *, *, #2910, .T. ) ;
#5884=EDGE_CURVE ( 'NONE', #10459, #9911, #5021, .T. ) ;
#5889=CYLINDRICAL_SURFACE ( 'NONE', #12038, 7.200000000007202416 ) ;
#5898=ADVANCED_FACE ( 'NONE', ( #7934 ), #6882, .T. ) ;
#5901=CARTESIAN_POINT ( 'NONE',  ( 4.999999999999999112, -11.41582255376066968, -8.527191590521194797 ) ) ;
#5905=CARTESIAN_POINT ( 'NONE',  ( 4.999999999999999112, 0.000000000000000000, 0.000000000000000000 ) ) ;
#5906=CYLINDRICAL_SURFACE ( 'NONE', #10604, 14.24900000001425227 ) ;
#5909=AXIS2_PLACEMENT_3D ( 'NONE', #11861, #5368, #6365 ) ;
#5910=ORIENTED_EDGE ( 'NONE', *, *, #125, .T. ) ;
#5917=VERTEX_POINT ( 'NONE', #348 ) ;
#5921=ADVANCED_FACE ( 'NONE', ( #10620 ), #6932, .T. ) ;
#5923=VERTEX_POINT ( 'NONE', #2164 ) ;
#5927=DIRECTION ( 'NONE',  ( -1.000000000000000000, 0.000000000000000000, 0.000000000000000000 ) ) ;
#5928=ORIENTED_EDGE ( 'NONE', *, *, #8460, .T. ) ;
#5932=ORIENTED_EDGE ( 'NONE', *, *, #2402, .F. ) ;
#5936=DIRECTION ( 'NONE',  ( -1.000000000000000000, 0.000000000000000000, 0.000000000000000000 ) ) ;
#5947=ORIENTED_EDGE ( 'NONE', *, *, #12009, .T. ) ;
#5969=FACE_OUTER_BOUND ( 'NONE', #12224, .T. ) ;
#5971=ORIENTED_EDGE ( 'NONE', *, *, #725, .T. ) ;
#5976=DIRECTION ( 'NONE',  ( -1.000000000000000000, 0.000000000000000000, 0.000000000000000000 ) ) ;
#5977=ORIENTED_EDGE ( 'NONE', *, *, #9917, .T. ) ;
#5982=EDGE_LOOP ( 'NONE', ( #5740, #5559, #10057, #1052 ) ) ;
#5983=AXIS2_PLACEMENT_3D ( 'NONE', #11507, #4652, #10575 ) ;
#5984=VERTEX_POINT ( 'NONE', #8178 ) ;
#5989=EDGE_LOOP ( 'NONE', ( #4518, #7697, #3172, #5788 ) ) ;
#5990=DIRECTION ( 'NONE',  ( 0.000000000000000000, -0.5000000000000072164, 0.8660254037844345998 ) ) ;
#6004=DIRECTION ( 'NONE',  ( 0.000000000000000000, 0.000000000000000000, 1.000000000000000000 ) ) ;
#6006=ORIENTED_EDGE ( 'NONE', *, *, #1519, .F. ) ;
#6022=CARTESIAN_POINT ( 'NONE',  ( 2.499999999999998668, 20.13931372320397273, -5.950465759858654557 ) ) ;
#6024=ORIENTED_EDGE ( 'NONE', *, *, #2116, .T. ) ;
#6029=CYLINDRICAL_SURFACE ( 'NONE', #8636, 21.00000000002100009 ) ;
#6037=FACE_OUTER_BOUND ( 'NONE', #11509, .T. ) ;
#6046=CIRCLE ( 'NONE', #2242, 7.200000000007202416 ) ;
#6050=DIRECTION ( 'NONE',  ( 0.000000000000000000, 0.000000000000000000, 1.000000000000000000 ) ) ;
#6055=VERTEX_POINT ( 'NONE', #8069 ) ;
#6056=AXIS2_PLACEMENT_3D ( 'NONE', #212, #4035, #8864 ) ;
#6060=DIRECTION ( 'NONE',  ( 1.000000000000000000, 0.000000000000000000, 0.000000000000000000 ) ) ;
#6070=DIRECTION ( 'NONE',  ( -1.000000000000000000, -0.000000000000000000, -0.000000000000000000 ) ) ;
#6091=EDGE_CURVE ( 'NONE', #9587, #3084, #3357, .T. ) ;
#6101=EDGE_LOOP ( 'NONE', ( #7331, #2744, #8546, #5255 ) ) ;
#6106=DIRECTION ( 'NONE',  ( 0.000000000000000000, 0.000000000000000000, 1.000000000000000000 ) ) ;
#6132=CYLINDRICAL_SURFACE ( 'NONE', #3256, 7.200000000007204193 ) ;
#6137=CARTESIAN_POINT ( 'NONE',  ( 0.000000000000000000, 0.000000000000000000, -1.500000000000000000 ) ) ;
#6138=ORIENTED_EDGE ( 'NONE', *, *, #498, .F. ) ;
#6142=DIRECTION ( 'NONE',  ( -1.000000000000000000, 0.000000000000000000, 0.000000000000000000 ) ) ;
#6148=ORIENTED_EDGE ( 'NONE', *, *, #7490, .T. ) ;
#6151=ADVANCED_FACE ( 'NONE', ( #11409 ), #7545, .T. ) ;
#6160=CYLINDRICAL_SURFACE ( 'NONE', #8036, 5.000000000000000000 ) ;
#6177=ADVANCED_FACE ( 'NONE', ( #9308 ), #4538, .T. ) ;
#6186=CARTESIAN_POINT ( 'NONE',  ( 4.999999999999999112, 0.000000000000000000, 0.000000000000000000 ) ) ;
#6193=DIRECTION ( 'NONE',  ( 1.000000000000000000, 0.000000000000000000, 0.000000000000000000 ) ) ;
#6214=DIRECTION ( 'NONE',  ( 0.000000000000000000, 0.000000000000000000, 1.000000000000000000 ) ) ;
#6219=CIRCLE ( 'NONE', #6826, 7.200000000007202416 ) ;
#6229=DIRECTION ( 'NONE',  ( -1.000000000000000000, 0.000000000000000000, -0.000000000000000000 ) ) ;
#6235=CARTESIAN_POINT ( 'NONE',  ( 4.999999999999999112, 11.41582255376072830, 8.527191590521114861 ) ) ;
#6242=EDGE_CURVE ( 'NONE', #1333, #10309, #5017, .T. ) ;
#6252=ORIENTED_EDGE ( 'NONE', *, *, #2884, .F. ) ;
#6256=( NAMED_UNIT ( * ) PLANE_ANGLE_UNIT ( ) SI_UNIT ( $, .RADIAN. ) );
#6259=CARTESIAN_POINT ( 'NONE',  ( 4.999999999999999112, 14.40062958310465469, -1.672489362011036595 ) ) ;
#6269=CIRCLE ( 'NONE', #7278, 7.200000000007200640 ) ;
#6274=ADVANCED_FACE ( 'NONE', ( #1323 ), #6029, .T. ) ;
#6282=CARTESIAN_POINT ( 'NONE',  ( 4.999999999999999112, 20.13931372320397273, -5.950465759858656334 ) ) ;
#6287=ORIENTED_EDGE ( 'NONE', *, *, #12029, .F. ) ;
#6298=DIRECTION ( 'NONE',  ( -1.000000000000000000, -0.000000000000000000, 0.000000000000000000 ) ) ;
#6300=LINE ( 'NONE', #2665, #4070 ) ;
#6306=CARTESIAN_POINT ( 'NONE',  ( 4.999999999999999112, 0.000000000000000000, 0.000000000000000000 ) ) ;
#6308=CARTESIAN_POINT ( 'NONE',  ( 4.999999999999999112, 0.000000000000000000, 0.000000000000000000 ) ) ;
#6309=EDGE_CURVE ( 'NONE', #5984, #5745, #2380, .T. ) ;
#6311=DIRECTION ( 'NONE',  ( 0.000000000000000000, 0.8660254037844398178, -0.4999999999999978906 ) ) ;
#6319=CARTESIAN_POINT ( 'NONE',  ( 4.999999999999999112, 16.90755573046746107, -0.4834863907626340551 ) ) ;
#6329=ORIENTED_EDGE ( 'NONE', *, *, #9232, .F. ) ;
#6348=LINE ( 'NONE', #11278, #8633 ) ;
#6358=ORIENTED_EDGE ( 'NONE', *, *, #11430, .F. ) ;
#6365=DIRECTION ( 'NONE',  ( 0.000000000000000000, 0.000000000000000000, 1.000000000000000000 ) ) ;
#6372=EDGE_CURVE ( 'NONE', #9803, #8928, #11930, .T. ) ;
#6381=CARTESIAN_POINT ( 'NONE',  ( -10.00000000000000000, 0.000000000000000000, 0.000000000000000000 ) ) ;
#6382=AXIS2_PLACEMENT_3D ( 'NONE', #4190, #8905, #7087 ) ;
#6387=CARTESIAN_POINT ( 'NONE',  ( 4.999999999999999112, 15.22291137398942240, -14.46592441914948779 ) ) ;
#6389=EDGE_CURVE ( 'NONE', #9911, #4914, #4630, .T. ) ;
#6399=EDGE_LOOP ( 'NONE', ( #10921, #4052, #9557, #11336 ) ) ;
#6400=CARTESIAN_POINT ( 'NONE',  ( 0.000000000000000000, 0.000000000000000000, 0.000000000000000000 ) ) ;
#6410=DIRECTION ( 'NONE',  ( 1.000000000000000000, -0.000000000000000000, 0.000000000000000000 ) ) ;
#6418=AXIS2_PLACEMENT_3D ( 'NONE', #9614, #9550, #11529 ) ;
#6429=AXIS2_PLACEMENT_3D ( 'NONE', #7037, #11764, #3220 ) ;
#6432=DIRECTION ( 'NONE',  ( 0.000000000000000000, 1.000000000000000000, 3.373073425507084106E-15 ) ) ;
#6433=VERTEX_POINT ( 'NONE', #562 ) ;
#6434=( GEOMETRIC_REPRESENTATION_CONTEXT ( 3 ) GLOBAL_UNCERTAINTY_ASSIGNED_CONTEXT ( ( #5655 ) ) GLOBAL_UNIT_ASSIGNED_CONTEXT ( ( #8131, #2606, #9998 ) ) REPRESENTATION_CONTEXT ( 'NONE', 'WORKASPACE' ) );
#6436=AXIS2_PLACEMENT_3D ( 'NONE', #1210, #3848, #4959 ) ;
#6441=VERTEX_POINT ( 'NONE', #6387 ) ;
#6442=DIRECTION ( 'NONE',  ( 0.000000000000000000, -0.5000000000000072164, 0.8660254037844345998 ) ) ;
#6449=CARTESIAN_POINT ( 'NONE',  ( 4.999999999999999112, 0.000000000000000000, 0.000000000000000000 ) ) ;
#6453=CARTESIAN_POINT ( 'NONE',  ( 4.999999999999999112, 5.950465759859149273, -20.13931372320382351 ) ) ;
#6463=DIRECTION ( 'NONE',  ( -1.000000000000000000, 0.000000000000000000, 0.000000000000000000 ) ) ;
#6468=ORIENTED_EDGE ( 'NONE', *, *, #1734, .F. ) ;
#6481=DIRECTION ( 'NONE',  ( -1.000000000000000000, -0.000000000000000000, -0.000000000000000000 ) ) ;
#6484=ORIENTED_EDGE ( 'NONE', *, *, #5478, .F. ) ;
#6485=AXIS2_PLACEMENT_3D ( 'NONE', #830, #12261, #1839 ) ;
#6494=ORIENTED_EDGE ( 'NONE', *, *, #324, .F. ) ;
#6505=CYLINDRICAL_SURFACE ( 'NONE', #3363, 7.200000000007202416 ) ;
#6507=CARTESIAN_POINT ( 'NONE',  ( 0.000000000000000000, -8.527191590521155717, 11.41582255376070343 ) ) ;
#6508=DIRECTION ( 'NONE',  ( -1.000000000000000000, 0.000000000000000000, -0.000000000000000000 ) ) ;
#6511=CARTESIAN_POINT ( 'NONE',  ( 50.00005079999999680, 4.769696007084728073, -1.500000000000000000 ) ) ;
#6512=DIRECTION ( 'NONE',  ( -1.000000000000000000, 0.000000000000000000, 0.000000000000000000 ) ) ;
#6514=ORIENTED_EDGE ( 'NONE', *, *, #4924, .T. ) ;
#6522=CARTESIAN_POINT ( 'NONE',  ( 0.000000000000000000, 14.40062958310465469, 8.872489362018239234 ) ) ;
#6524=FACE_OUTER_BOUND ( 'NONE', #111, .T. ) ;
#6525=CYLINDRICAL_SURFACE ( 'NONE', #5818, 7.200000000007202416 ) ;
#6527=DIRECTION ( 'NONE',  ( -1.000000000000000000, 0.000000000000000000, -0.000000000000000000 ) ) ;
#6529=EDGE_CURVE ( 'NONE', #7347, #9806, #8576, .T. ) ;
#6536=EDGE_LOOP ( 'NONE', ( #12191, #10087, #604, #10107 ) ) ;
#6537=DIRECTION ( 'NONE',  ( 0.000000000000000000, -0.8660254037844433705, 0.4999999999999920064 ) ) ;
#6543=DIRECTION ( 'NONE',  ( -1.000000000000000000, 0.000000000000000000, 0.000000000000000000 ) ) ;
#6554=CARTESIAN_POINT ( 'NONE',  ( 5.000000000000000000, 0.000000000000000000, 0.000000000000000000 ) ) ;
#6561=CIRCLE ( 'NONE', #2563, 7.200000000007202416 ) ;
#6567=CARTESIAN_POINT ( 'NONE',  ( 4.999999999999999112, -16.90755573046745752, 6.716513609244448624 ) ) ;
#6577=DIRECTION ( 'NONE',  ( 0.000000000000000000, 0.000000000000000000, 1.000000000000000000 ) ) ;
#6613=VERTEX_POINT ( 'NONE', #8706 ) ;
#6615=ADVANCED_BREP_SHAPE_REPRESENTATION ( '', ( #8493, #6056 ), #6434 ) ;
#6618=CARTESIAN_POINT ( 'NONE',  ( 2.499999999999998668, 5.950465759858869497, 20.13931372320390523 ) ) ;
#6630=CIRCLE ( 'NONE', #3618, 7.200000000007203305 ) ;
#6640=AXIS2_PLACEMENT_3D ( 'NONE', #12324, #3778, #7597 ) ;
#6643=CARTESIAN_POINT ( 'NONE',  ( 4.999999999999999112, 5.622796541391749336, -13.09267581720861173 ) ) ;
#6685=ORIENTED_EDGE ( 'NONE', *, *, #12127, .T. ) ;
#6689=DIRECTION ( 'NONE',  ( 0.000000000000000000, -6.982962677686266711E-15, 1.000000000000000000 ) ) ;
#6693=CARTESIAN_POINT ( 'NONE',  ( 4.999999999999999112, 16.90755573046746107, -0.4834863907626340551 ) ) ;
#6696=CARTESIAN_POINT ( 'NONE',  ( -10.00000000000000000, 0.000000000000000000, 0.000000000000000000 ) ) ;
#6698=EDGE_LOOP ( 'NONE', ( #7983, #5856, #11056, #917 ) ) ;
#6701=EDGE_CURVE ( 'NONE', #6441, #5917, #8182, .T. ) ;
#6703=VECTOR ( 'NONE', #3082, 1000.000000000000000 ) ;
#6710=FACE_OUTER_BOUND ( 'NONE', #10314, .T. ) ;
#6711=ORIENTED_EDGE ( 'NONE', *, *, #11864, .T. ) ;
#6715=CARTESIAN_POINT ( 'NONE',  ( 4.999999999999999112, 0.000000000000000000, 0.000000000000000000 ) ) ;
#6716=EDGE_CURVE ( 'NONE', #3733, #11755, #10927, .T. ) ;
#6735=DIRECTION ( 'NONE',  ( 0.000000000000000000, 0.000000000000000000, 1.000000000000000000 ) ) ;
#6737=CYLINDRICAL_SURFACE ( 'NONE', #8476, 14.24900000001425227 ) ;
#6760=EDGE_CURVE ( 'NONE', #420, #3401, #386, .T. ) ;
#6761=ORIENTED_EDGE ( 'NONE', *, *, #6858, .F. ) ;
#6762=CARTESIAN_POINT ( 'NONE',  ( 4.999999999999999112, 11.41582255376084909, -8.527191590520953213 ) ) ;
#6771=FACE_OUTER_BOUND ( 'NONE', #5517, .T. ) ;
#6797=VECTOR ( 'NONE', #8315, 1000.000000000000000 ) ;
#6799=ORIENTED_EDGE ( 'NONE', *, *, #4699, .F. ) ;
#6800=ORIENTED_EDGE ( 'NONE', *, *, #4244, .T. ) ;
#6805=CIRCLE ( 'NONE', #5584, 21.00000000002100009 ) ;
#6814=CARTESIAN_POINT ( 'NONE',  ( 4.999999999999999112, 8.872489362018390224, -14.40062958310456054 ) ) ;
#6815=ORIENTED_EDGE ( 'NONE', *, *, #9151, .F. ) ;
#6824=AXIS2_PLACEMENT_3D ( 'NONE', #3143, #2309, #10754 ) ;
#6826=AXIS2_PLACEMENT_3D ( 'NONE', #3836, #9719, #5762 ) ;
#6834=CIRCLE ( 'NONE', #11606, 14.24900000001425404 ) ;
#6836=PRODUCT ( 'spur gear_iso_ISO - Spur gear 3M 12T 20PA 5FW ---S12A75H50L10.0S1', 'spur gear_iso_ISO - Spur gear 3M 12T 20PA 5FW ---S12A75H50L10.0S1', '', ( #5538 ) ) ;
#6855=AXIS2_PLACEMENT_3D ( 'NONE', #11521, #10666, #9791 ) ;
#6858=EDGE_CURVE ( 'NONE', #661, #3785, #3788, .T. ) ;
#6860=LINE ( 'NONE', #2093, #1441 ) ;
#6882=CYLINDRICAL_SURFACE ( 'NONE', #11597, 14.24900000001425227 ) ;
#6886=EDGE_CURVE ( 'NONE', #4099, #3713, #5441, .T. ) ;
#6893=CIRCLE ( 'NONE', #7485, 7.200000000007200640 ) ;
#6897=ORIENTED_EDGE ( 'NONE', *, *, #4580, .F. ) ;
#6921=EDGE_CURVE ( 'NONE', #3765, #8559, #9783, .T. ) ;
#6932=CYLINDRICAL_SURFACE ( 'NONE', #7031, 7.200000000007202416 ) ;
#6942=LINE ( 'NONE', #7755, #9266 ) ;
#6943=ORIENTED_EDGE ( 'NONE', *, *, #1496, .F. ) ;
#6947=EDGE_CURVE ( 'NONE', #9895, #3834, #4556, .T. ) ;
#6953=CARTESIAN_POINT ( 'NONE',  ( 4.999999999999999112, 4.916402349214867407, -20.41639017900854469 ) ) ;
#6968=CIRCLE ( 'NONE', #1569, 14.24900000001425227 ) ;
#6975=ORIENTED_EDGE ( 'NONE', *, *, #2910, .F. ) ;
#6980=CYLINDRICAL_SURFACE ( 'NONE', #10607, 7.200000000007202416 ) ;
#6983=CIRCLE ( 'NONE', #1997, 5.000000000000000000 ) ;
#6994=ADVANCED_FACE ( 'NONE', ( #867 ), #6505, .T. ) ;
#6997=DIRECTION ( 'NONE',  ( -1.000000000000000000, -0.000000000000000000, 0.000000000000000000 ) ) ;
#7003=AXIS2_PLACEMENT_3D ( 'NONE', #5393, #11260, #7214 ) ;
#7004=CARTESIAN_POINT ( 'NONE',  ( 0.000000000000000000, 0.000000000000000000, 0.000000000000000000 ) ) ;
#7022=ORIENTED_EDGE ( 'NONE', *, *, #7887, .T. ) ;
#7031=AXIS2_PLACEMENT_3D ( 'NONE', #10734, #2060, #1236 ) ;
#7037=CARTESIAN_POINT ( 'NONE',  ( 0.000000000000000000, -14.88411597386723351, -8.035066368449358620 ) ) ;
#7040=EDGE_LOOP ( 'NONE', ( #10191, #9049, #6897, #6329 ) ) ;
#7048=CIRCLE ( 'NONE', #10845, 7.200000000007202416 ) ;
#7050=CARTESIAN_POINT ( 'NONE',  ( 0.000000000000000000, 0.000000000000000000, 0.000000000000000000 ) ) ;
#7051=DIRECTION ( 'NONE',  ( 0.000000000000000000, 0.000000000000000000, 1.000000000000000000 ) ) ;
#7054=ORIENTED_EDGE ( 'NONE', *, *, #1272, .T. ) ;
#7064=EDGE_CURVE ( 'NONE', #3765, #611, #9956, .T. ) ;
#7077=DIRECTION ( 'NONE',  ( 1.000000000000000000, 0.000000000000000000, -0.000000000000000000 ) ) ;
#7085=ORIENTED_EDGE ( 'NONE', *, *, #4761, .T. ) ;
#7086=ORIENTED_EDGE ( 'NONE', *, *, #4088, .F. ) ;
#7087=DIRECTION ( 'NONE',  ( 0.000000000000000000, -0.8660254037844328234, -0.5000000000000101030 ) ) ;
#7088=DIRECTION ( 'NONE',  ( 0.000000000000000000, -1.000000000000000000, 0.000000000000000000 ) ) ;
#7095=EDGE_CURVE ( 'NONE', #611, #2076, #929, .T. ) ;
#7096=EDGE_CURVE ( 'NONE', #10859, #1263, #5556, .T. ) ;
#7105=ORIENTED_EDGE ( 'NONE', *, *, #6372, .F. ) ;
#7108=ORIENTED_EDGE ( 'NONE', *, *, #547, .F. ) ;
#7109=CIRCLE ( 'NONE', #1912, 7.200000000007202416 ) ;
#7118=ORIENTED_EDGE ( 'NONE', *, *, #6716, .F. ) ;
#7129=ORIENTED_EDGE ( 'NONE', *, *, #12009, .F. ) ;
#7136=DIRECTION ( 'NONE',  ( -1.000000000000000000, -0.000000000000000000, 0.000000000000000000 ) ) ;
#7146=DIRECTION ( 'NONE',  ( 0.000000000000000000, 0.000000000000000000, 1.000000000000000000 ) ) ;
#7163=CIRCLE ( 'NONE', #10943, 7.200000000007204193 ) ;
#7168=FACE_OUTER_BOUND ( 'NONE', #4870, .T. ) ;
#7171=EDGE_CURVE ( 'NONE', #12241, #4691, #3248, .T. ) ;
#7181=CARTESIAN_POINT ( 'NONE',  ( 4.999999999999999112, -8.035066368449101049, -14.88411597386737562 ) ) ;
#7187=AXIS2_PLACEMENT_3D ( 'NONE', #7923, #3164, #6106 ) ;
#7188=CARTESIAN_POINT ( 'NONE',  ( 0.000000000000000000, 14.46592441914986082, -15.22291137398907068 ) ) ;
#7200=VECTOR ( 'NONE', #4086, 1000.000000000000000 ) ;
#7204=CARTESIAN_POINT ( 'NONE',  ( 4.999999999999999112, -0.4834863907624570856, -16.90755573046746463 ) ) ;
#7214=DIRECTION ( 'NONE',  ( 0.000000000000000000, 0.000000000000000000, 1.000000000000000000 ) ) ;
#7226=DIRECTION ( 'NONE',  ( -1.000000000000000000, -0.000000000000000000, 0.000000000000000000 ) ) ;
#7227=AXIS2_PLACEMENT_3D ( 'NONE', #402, #4222, #11846 ) ;
#7229=AXIS2_PLACEMENT_3D ( 'NONE', #9627, #1060, #8808 ) ;
#7233=AXIS2_PLACEMENT_3D ( 'NONE', #2713, #6481, #8415 ) ;
#7237=EDGE_CURVE ( 'NONE', #10134, #3460, #7163, .T. ) ;
#7240=DIRECTION ( 'NONE',  ( 0.000000000000000000, 0.4999999999999948930, 0.8660254037844414832 ) ) ;
#7242=ADVANCED_FACE ( 'NONE', ( #2534 ), #9181, .T. ) ;
#7250=CARTESIAN_POINT ( 'NONE',  ( 2.499999999999999556, -14.46592441914974714, 15.22291137398917193 ) ) ;
#7251=AXIS2_PLACEMENT_3D ( 'NONE', #7572, #4751, #7645 ) ;
#7256=CARTESIAN_POINT ( 'NONE',  ( 4.999999999999999112, -14.88411597386734897, 8.035066368449154339 ) ) ;
#7261=AXIS2_PLACEMENT_3D ( 'NONE', #2621, #8319, #5508 ) ;
#7271=DIRECTION ( 'NONE',  ( -1.000000000000000000, 0.000000000000000000, 0.000000000000000000 ) ) ;
#7278=AXIS2_PLACEMENT_3D ( 'NONE', #12278, #12215, #10228 ) ;
#7279=DIRECTION ( 'NONE',  ( -1.000000000000000000, 0.000000000000000000, 0.000000000000000000 ) ) ;
#7289=ORIENTED_EDGE ( 'NONE', *, *, #11505, .F. ) ;
#7290=FACE_OUTER_BOUND ( 'NONE', #6101, .T. ) ;
#7296=EDGE_LOOP ( 'NONE', ( #8622, #2379, #8527, #7484 ) ) ;
#7298=CARTESIAN_POINT ( 'NONE',  ( 4.999999999999999112, 0.000000000000000000, 0.000000000000000000 ) ) ;
#7305=ORIENTED_EDGE ( 'NONE', *, *, #8217, .T. ) ;
#7309=EDGE_LOOP ( 'NONE', ( #9051, #11389, #9704, #8276 ) ) ;
#7321=ADVANCED_FACE ( 'NONE', ( #538 ), #5426, .T. ) ;
#7324=DIRECTION ( 'NONE',  ( -1.000000000000000000, 0.000000000000000000, 0.000000000000000000 ) ) ;
#7325=EDGE_CURVE ( 'NONE', #4584, #3417, #764, .T. ) ;
#7326=CARTESIAN_POINT ( 'NONE',  ( 4.999999999999999112, -13.09267581720863127, -5.622796541391703151 ) ) ;
#7331=ORIENTED_EDGE ( 'NONE', *, *, #9060, .T. ) ;
#7340=CARTESIAN_POINT ( 'NONE',  ( 2.499999999999999556, -5.950465759859009829, 20.13931372320386259 ) ) ;
#7347=VERTEX_POINT ( 'NONE', #7361 ) ;
#7350=CARTESIAN_POINT ( 'NONE',  ( 2.499999999999999556, 14.46592441914986082, -15.22291137398907068 ) ) ;
#7352=DIRECTION ( 'NONE',  ( -1.000000000000000000, -0.000000000000000000, -0.000000000000000000 ) ) ;
#7361=CARTESIAN_POINT ( 'NONE',  ( 4.999999999999999112, 11.41582255376084909, -8.527191590520953213 ) ) ;
#7362=AXIS2_PLACEMENT_3D ( 'NONE', #6186, #685, #5503 ) ;
#7376=AXIS2_PLACEMENT_3D ( 'NONE', #706, #10146, #1580 ) ;
#7387=CARTESIAN_POINT ( 'NONE',  ( 4.999999999999999112, 0.000000000000000000, 0.000000000000000000 ) ) ;
#7395=VECTOR ( 'NONE', #10047, 1000.000000000000000 ) ;
#7396=CARTESIAN_POINT ( 'NONE',  ( 0.000000000000000000, 16.90755573046746107, 6.716513609244568528 ) ) ;
#7397=DIRECTION ( 'NONE',  ( -1.000000000000000000, -0.000000000000000000, -0.000000000000000000 ) ) ;
#7402=PRODUCT_DEFINITION ( 'UNKNOWN', '', #3251, #4263 ) ;
#7404=DIRECTION ( 'NONE',  ( -1.000000000000000000, -0.000000000000000000, 0.000000000000000000 ) ) ;
#7408=STYLED_ITEM('',(#12412),#8493);
#7414=DIRECTION ( 'NONE',  ( 0.000000000000000000, 0.000000000000000000, 1.000000000000000000 ) ) ;
#7417=CIRCLE ( 'NONE', #416, 5.000000000000000000 ) ;
#7427=CARTESIAN_POINT ( 'NONE',  ( 4.999999999999999112, -16.90755573046746463, 0.4834863907625160939 ) ) ;
#7441=CARTESIAN_POINT ( 'NONE',  ( 0.000000000000000000, -8.035066368449308882, 14.88411597386726193 ) ) ;
#7442=VERTEX_POINT ( 'NONE', #12337 ) ;
#7448=CARTESIAN_POINT ( 'NONE',  ( 0.000000000000000000, 16.90755573046745397, 0.4834863907628708102 ) ) ;
#7451=VERTEX_POINT ( 'NONE', #11411 ) ;
#7459=VECTOR ( 'NONE', #7705, 1000.000000000000000 ) ;
#7470=DIRECTION ( 'NONE',  ( -1.000000000000000000, 0.000000000000000000, -0.000000000000000000 ) ) ;
#7479=CYLINDRICAL_SURFACE ( 'NONE', #1396, 21.00000000002100009 ) ;
#7484=ORIENTED_EDGE ( 'NONE', *, *, #4016, .F. ) ;
#7485=AXIS2_PLACEMENT_3D ( 'NONE', #5524, #9344, #2464 ) ;
#7487=ORIENTED_EDGE ( 'NONE', *, *, #6947, .F. ) ;
#7488=FACE_OUTER_BOUND ( 'NONE', #8100, .T. ) ;
#7490=EDGE_CURVE ( 'NONE', #1263, #4341, #7975, .T. ) ;
#7492=ADVANCED_FACE ( 'NONE', ( #3469 ), #11139, .T. ) ;
#7498=CARTESIAN_POINT ( 'NONE',  ( 0.000000000000000000, -4.916402349214440193, -20.41639017900864772 ) ) ;
#7503=FACE_OUTER_BOUND ( 'NONE', #11566, .T. ) ;
#7513=DIRECTION ( 'NONE',  ( 0.000000000000000000, 0.000000000000000000, 1.000000000000000000 ) ) ;
#7518=CYLINDRICAL_SURFACE ( 'NONE', #12177, 14.24900000001425227 ) ;
#7533=EDGE_CURVE ( 'NONE', #403, #6433, #7773, .T. ) ;
#7545=CYLINDRICAL_SURFACE ( 'NONE', #9020, 7.200000000007200640 ) ;
#7551=DIRECTION ( 'NONE',  ( 1.000000000000000000, -0.000000000000000000, -0.000000000000000000 ) ) ;
#7558=DIRECTION ( 'NONE',  ( -1.000000000000000000, -0.000000000000000000, -0.000000000000000000 ) ) ;
#7562=ADVANCED_FACE ( 'NONE', ( #7290 ), #2516, .T. ) ;
#7566=AXIS2_PLACEMENT_3D ( 'NONE', #9668, #1091, #12270 ) ;
#7572=CARTESIAN_POINT ( 'NONE',  ( 4.999999999999999112, 16.90755573046745397, 0.4834863907628708102 ) ) ;
#7573=LINE ( 'NONE', #10313, #3690 ) ;
#7577=AXIS2_PLACEMENT_3D ( 'NONE', #10615, #11533, #3741 ) ;
#7582=AXIS2_PLACEMENT_3D ( 'NONE', #5578, #7719, #826 ) ;
#7585=CARTESIAN_POINT ( 'NONE',  ( 4.999999999999997335, 0.000000000000000000, 0.000000000000000000 ) ) ;
#7591=AXIS2_PLACEMENT_3D ( 'NONE', #9921, #9114, #9056 ) ;
#7592=EDGE_CURVE ( 'NONE', #5277, #9895, #12348, .T. ) ;
#7597=DIRECTION ( 'NONE',  ( 0.000000000000000000, -0.4999999999999888978, -0.8660254037844450359 ) ) ;
#7599=ORIENTED_EDGE ( 'NONE', *, *, #9150, .T. ) ;
#7606=ORIENTED_EDGE ( 'NONE', *, *, #1519, .T. ) ;
#7608=DIRECTION ( 'NONE',  ( -1.000000000000000000, 0.000000000000000000, 0.000000000000000000 ) ) ;
#7621=DIRECTION ( 'NONE',  ( 0.000000000000000000, 0.000000000000000000, 1.000000000000000000 ) ) ;
#7628=CARTESIAN_POINT ( 'NONE',  ( 0.000000000000000000, 6.799999999999999822, 1.500000000000000000 ) ) ;
#7631=EDGE_LOOP ( 'NONE', ( #7289, #3171, #10682, #11464, #7086, #6815 ) ) ;
#7636=AXIS2_PLACEMENT_3D ( 'NONE', #12138, #7352, #7414 ) ;
#7645=DIRECTION ( 'NONE',  ( 0.000000000000000000, -0.4999999999999888423, -0.8660254037844451469 ) ) ;
#7650=ADVANCED_FACE ( 'NONE', ( #6524 ), #3899, .F. ) ;
#7663=DIRECTION ( 'NONE',  ( 1.000000000000000000, 0.000000000000000000, 0.000000000000000000 ) ) ;
#7672=DIRECTION ( 'NONE',  ( 0.000000000000000000, 0.000000000000000000, 1.000000000000000000 ) ) ;
#7687=DIRECTION ( 'NONE',  ( -1.000000000000000000, -0.000000000000000000, 0.000000000000000000 ) ) ;
#7689=EDGE_CURVE ( 'NONE', #8093, #10792, #1384, .T. ) ;
#7691=LINE ( 'NONE', #5610, #2172 ) ;
#7697=ORIENTED_EDGE ( 'NONE', *, *, #10444, .T. ) ;
#7705=DIRECTION ( 'NONE',  ( -1.000000000000000000, 0.000000000000000000, 0.000000000000000000 ) ) ;
#7706=EDGE_CURVE ( 'NONE', #9748, #2794, #7781, .T. ) ;
#7716=FACE_OUTER_BOUND ( 'NONE', #7932, .T. ) ;
#7717=DIRECTION ( 'NONE',  ( 1.000000000000000000, 0.000000000000000000, 0.000000000000000000 ) ) ;
#7719=DIRECTION ( 'NONE',  ( -1.000000000000000000, 0.000000000000000000, 0.000000000000000000 ) ) ;
#7726=ADVANCED_FACE ( 'NONE', ( #6771 ), #5837, .T. ) ;
#7729=FACE_OUTER_BOUND ( 'NONE', #6536, .T. ) ;
#7737=ORIENTED_EDGE ( 'NONE', *, *, #8255, .F. ) ;
#7741=CARTESIAN_POINT ( 'NONE',  ( 4.999999999999999112, 8.527191590521072229, 11.41582255376076027 ) ) ;
#7742=DIRECTION ( 'NONE',  ( 0.000000000000000000, 0.8660254037844398178, -0.4999999999999980571 ) ) ;
#7745=ORIENTED_EDGE ( 'NONE', *, *, #8938, .F. ) ;
#7746=ORIENTED_EDGE ( 'NONE', *, *, #305, .T. ) ;
#7748=ORIENTED_EDGE ( 'NONE', *, *, #11783, .T. ) ;
#7752=ADVANCED_FACE ( 'NONE', ( #3653 ), #8, .T. ) ;
#7755=CARTESIAN_POINT ( 'NONE',  ( 5.000000000000000000, 6.799999999999999822, 0.000000000000000000 ) ) ;
#7762=EDGE_CURVE ( 'NONE', #542, #1039, #6983, .T. ) ;
#7763=EDGE_CURVE ( 'NONE', #1039, #6055, #11450, .T. ) ;
#7765=ADVANCED_FACE ( 'NONE', ( #8841, #1374 ), #11639, .F. ) ;
#7773=CIRCLE ( 'NONE', #2170, 14.24900000001425049 ) ;
#7781=CIRCLE ( 'NONE', #5983, 14.24900000001425227 ) ;
#7789=CYLINDRICAL_SURFACE ( 'NONE', #5053, 21.00000000002100009 ) ;
#7790=EDGE_LOOP ( 'NONE', ( #6685, #2057, #5932, #3792 ) ) ;
#7797=EDGE_CURVE ( 'NONE', #11913, #661, #9377, .T. ) ;
#7802=CARTESIAN_POINT ( 'NONE',  ( 4.999999999999999112, -11.41582255376079047, 8.527191590521034925 ) ) ;
#7816=ORIENTED_EDGE ( 'NONE', *, *, #5787, .F. ) ;
#7817=DIRECTION ( 'NONE',  ( -1.000000000000000000, 0.000000000000000000, 0.000000000000000000 ) ) ;
#7841=CARTESIAN_POINT ( 'NONE',  ( 0.000000000000000000, 15.22291137398921990, 14.46592441914969918 ) ) ;
#7844=DIRECTION ( 'NONE',  ( 0.000000000000000000, 1.000000000000000000, 3.373073425507084106E-15 ) ) ;
#7850=AXIS2_PLACEMENT_3D ( 'NONE', #12034, #10161, #2529 ) ;
#7853=CARTESIAN_POINT ( 'NONE',  ( -10.00000000000000000, 0.000000000000000000, 0.000000000000000000 ) ) ;
#7861=ORIENTED_EDGE ( 'NONE', *, *, #2493, .T. ) ;
#7869=ADVANCED_FACE ( 'NONE', ( #10831 ), #11563, .T. ) ;
#7874=CARTESIAN_POINT ( 'NONE',  ( 4.999999999999999112, 16.90755573046746107, -0.4834863907626340551 ) ) ;
#7883=DIRECTION ( 'NONE',  ( 0.000000000000000000, -6.987080667121815555E-15, 1.000000000000000000 ) ) ;
#7887=EDGE_CURVE ( 'NONE', #10787, #9456, #2374, .T. ) ;
#7897=AXIS2_PLACEMENT_3D ( 'NONE', #11371, #2815, #11441 ) ;
#7902=VERTEX_POINT ( 'NONE', #9898 ) ;
#7904=DIRECTION ( 'NONE',  ( 0.000000000000000000, 0.000000000000000000, 1.000000000000000000 ) ) ;
#7908=ORIENTED_EDGE ( 'NONE', *, *, #6921, .T. ) ;
#7910=EDGE_CURVE ( 'NONE', #3410, #9763, #10651, .T. ) ;
#7912=CARTESIAN_POINT ( 'NONE',  ( 4.999999999999999112, 16.90755573046746107, 6.716513609244568528 ) ) ;
#7913=EDGE_CURVE ( 'NONE', #8750, #9528, #3380, .T. ) ;
#7914=DIRECTION ( 'NONE',  ( -1.000000000000000000, -0.000000000000000000, 0.000000000000000000 ) ) ;
#7915=DIRECTION ( 'NONE',  ( 0.000000000000000000, -1.000000000000000000, -1.036015409262890124E-14 ) ) ;
#7923=CARTESIAN_POINT ( 'NONE',  ( 4.999999999999999112, 0.000000000000000000, 0.000000000000000000 ) ) ;
#7926=DIRECTION ( 'NONE',  ( -1.000000000000000000, 0.000000000000000000, 0.000000000000000000 ) ) ;
#7931=ORIENTED_EDGE ( 'NONE', *, *, #3317, .F. ) ;
#7932=EDGE_LOOP ( 'NONE', ( #667, #1036, #4139, #9865 ) ) ;
#7934=FACE_OUTER_BOUND ( 'NONE', #6399, .T. ) ;
#7940=DIRECTION ( 'NONE',  ( 0.000000000000000000, -6.987080667121817133E-15, 1.000000000000000000 ) ) ;
#7947=ORIENTED_EDGE ( 'NONE', *, *, #2538, .T. ) ;
#7957=CARTESIAN_POINT ( 'NONE',  ( 50.00005079999999680, 6.123233995736766282E-16, -5.000000000000000000 ) ) ;
#7963=VECTOR ( 'NONE', #10524, 1000.000000000000000 ) ;
#7965=DIRECTION ( 'NONE',  ( -1.000000000000000000, 0.000000000000000000, 0.000000000000000000 ) ) ;
#7966=DIRECTION ( 'NONE',  ( 0.000000000000000000, 0.000000000000000000, 1.000000000000000000 ) ) ;
#7969=VECTOR ( 'NONE', #487, 1000.000000000000000 ) ;
#7975=CIRCLE ( 'NONE', #2569, 7.200000000007203305 ) ;
#7980=CARTESIAN_POINT ( 'NONE',  ( 4.999999999999999112, -5.950465759858725612, -20.13931372320394786 ) ) ;
#7983=ORIENTED_EDGE ( 'NONE', *, *, #5343, .T. ) ;
#7986=ORIENTED_EDGE ( 'NONE', *, *, #4227, .T. ) ;
#7990=AXIS2_PLACEMENT_3D ( 'NONE', #12268, #9834, #5658 ) ;
#7993=CARTESIAN_POINT ( 'NONE',  ( 4.999999999999999112, 13.09267581720866858, 5.622796541391611669 ) ) ;
#8004=CYLINDRICAL_SURFACE ( 'NONE', #5237, 7.200000000007202416 ) ;
#8024=VERTEX_POINT ( 'NONE', #2105 ) ;
#8034=DIRECTION ( 'NONE',  ( -1.000000000000000000, 0.000000000000000000, -0.000000000000000000 ) ) ;
#8036=AXIS2_PLACEMENT_3D ( 'NONE', #11898, #2340, #8169 ) ;
#8040=DIRECTION ( 'NONE',  ( 0.000000000000000000, 0.5000000000000009992, -0.8660254037844381525 ) ) ;
#8042=COLOUR_RGB ( '',1.000000000000000000, 0.9490196078431372140, 0.9098039215686274384 ) ;
#8055=VECTOR ( 'NONE', #10052, 1000.000000000000000 ) ;
#8057=DIRECTION ( 'NONE',  ( 1.000000000000000000, 0.000000000000000000, 0.000000000000000000 ) ) ;
#8060=DIRECTION ( 'NONE',  ( -1.000000000000000000, 0.000000000000000000, 0.000000000000000000 ) ) ;
#8069=CARTESIAN_POINT ( 'NONE',  ( 0.000000000000000000, 6.123233995736766282E-16, -5.000000000000000000 ) ) ;
#8077=ORIENTED_EDGE ( 'NONE', *, *, #10853, .T. ) ;
#8086=CARTESIAN_POINT ( 'NONE',  ( 4.999999999999999112, -5.622796541391473113, -13.09267581720872720 ) ) ;
#8092=EDGE_CURVE ( 'NONE', #26, #2796, #6805, .T. ) ;
#8093=VERTEX_POINT ( 'NONE', #1530 ) ;
#8100=EDGE_LOOP ( 'NONE', ( #3706, #11512, #9809, #4872 ) ) ;
#8106=CARTESIAN_POINT ( 'NONE',  ( 0.000000000000000000, -8.872489362018088244, -14.40062958310474883 ) ) ;
#8110=ORIENTED_EDGE ( 'NONE', *, *, #7689, .F. ) ;
#8112=ORIENTED_EDGE ( 'NONE', *, *, #3623, .F. ) ;
#8116=DIRECTION ( 'NONE',  ( 0.000000000000000000, 0.5000000000000008882, -0.8660254037844381525 ) ) ;
#8117=CARTESIAN_POINT ( 'NONE',  ( 4.999999999999999112, -13.09267581720870766, 5.622796541391519298 ) ) ;
#8118=CARTESIAN_POINT ( 'NONE',  ( 4.999999999999999112, -16.90755573046746463, 0.4834863907625160939 ) ) ;
#8123=EDGE_LOOP ( 'NONE', ( #8307, #6943, #7105, #5673 ) ) ;
#8125=DIRECTION ( 'NONE',  ( -1.000000000000000000, 0.000000000000000000, 0.000000000000000000 ) ) ;
#8127=CARTESIAN_POINT ( 'NONE',  ( 0.000000000000000000, -5.622796541391473113, -13.09267581720872720 ) ) ;
#8131=( LENGTH_UNIT ( ) NAMED_UNIT ( * ) SI_UNIT ( .MILLI., .METRE. ) );
#8140=DIRECTION ( 'NONE',  ( -1.000000000000000000, 0.000000000000000000, 0.000000000000000000 ) ) ;
#8143=DIRECTION ( 'NONE',  ( -1.000000000000000000, -0.000000000000000000, -0.000000000000000000 ) ) ;
#8151=EDGE_CURVE ( 'NONE', #10787, #8093, #10963, .T. ) ;
#8164=DIRECTION ( 'NONE',  ( 0.000000000000000000, 0.8660254037844362651, 0.5000000000000038858 ) ) ;
#8169=DIRECTION ( 'NONE',  ( 0.000000000000000000, 0.000000000000000000, 1.000000000000000000 ) ) ;
#8172=LINE ( 'NONE', #2475, #3064 ) ;
#8178=CARTESIAN_POINT ( 'NONE',  ( 4.999999999999997335, 6.799999999999999822, 1.500000000000000000 ) ) ;
#8179=DIRECTION ( 'NONE',  ( 0.000000000000000000, 0.000000000000000000, 1.000000000000000000 ) ) ;
#8182=CIRCLE ( 'NONE', #1186, 21.00000000002100009 ) ;
#8202=CARTESIAN_POINT ( 'NONE',  ( 2.499999999999998668, 4.916402349214582301, 20.41639017900861219 ) ) ;
#8217=EDGE_CURVE ( 'NONE', #9456, #3968, #12165, .T. ) ;
#8222=EDGE_LOOP ( 'NONE', ( #2716, #2689, #1526, #2291 ) ) ;
#8225=AXIS2_PLACEMENT_3D ( 'NONE', #1108, #4919, #8803 ) ;
#8232=FACE_OUTER_BOUND ( 'NONE', #9395, .T. ) ;
#8244=CYLINDRICAL_SURFACE ( 'NONE', #1671, 14.24900000001425227 ) ;
#8250=CIRCLE ( 'NONE', #647, 7.200000000007202416 ) ;
#8253=CARTESIAN_POINT ( 'NONE',  ( 0.000000000000000000, 8.872489362018189496, 14.40062958310468666 ) ) ;
#8254=ADVANCED_FACE ( 'NONE', ( #8232 ), #12027, .T. ) ;
#8255=EDGE_CURVE ( 'NONE', #12042, #8435, #4053, .T. ) ;
#8265=CIRCLE ( 'NONE', #9867, 5.000000000000000000 ) ;
#8267=EDGE_CURVE ( 'NONE', #5277, #10549, #8292, .T. ) ;
#8268=DIRECTION ( 'NONE',  ( 0.000000000000000000, 0.5000000000000008882, -0.8660254037844381525 ) ) ;
#8272=EDGE_LOOP ( 'NONE', ( #6468, #6287, #8077, #12143 ) ) ;
#8274=CIRCLE ( 'NONE', #869, 7.200000000007202416 ) ;
#8276=ORIENTED_EDGE ( 'NONE', *, *, #7064, .T. ) ;
#8278=ORIENTED_EDGE ( 'NONE', *, *, #8533, .F. ) ;
#8285=CARTESIAN_POINT ( 'NONE',  ( 0.000000000000000000, 0.000000000000000000, 0.000000000000000000 ) ) ;
#8286=ORIENTED_EDGE ( 'NONE', *, *, #946, .F. ) ;
#8287=CARTESIAN_POINT ( 'NONE',  ( 0.000000000000000000, 0.4834863907628118573, -16.90755573046745397 ) ) ;
#8292=LINE ( 'NONE', #656, #3203 ) ;
#8295=DIRECTION ( 'NONE',  ( -1.000000000000000000, 0.000000000000000000, 0.000000000000000000 ) ) ;
#8300=DIRECTION ( 'NONE',  ( 0.000000000000000000, 0.000000000000000000, 1.000000000000000000 ) ) ;
#8307=ORIENTED_EDGE ( 'NONE', *, *, #10535, .F. ) ;
#8312=SURFACE_STYLE_FILL_AREA ( #607 ) ;
#8315=DIRECTION ( 'NONE',  ( -1.000000000000000000, 0.000000000000000000, 0.000000000000000000 ) ) ;
#8317=CARTESIAN_POINT ( 'NONE',  ( 0.000000000000000000, 0.000000000000000000, 0.000000000000000000 ) ) ;
#8319=DIRECTION ( 'NONE',  ( -1.000000000000000000, -0.000000000000000000, 0.000000000000000000 ) ) ;
#8328=VERTEX_POINT ( 'NONE', #714 ) ;
#8332=DIRECTION ( 'NONE',  ( -1.000000000000000000, 0.000000000000000000, 0.000000000000000000 ) ) ;
#8338=DIRECTION ( 'NONE',  ( 0.000000000000000000, 0.000000000000000000, -1.000000000000000000 ) ) ;
#8347=ORIENTED_EDGE ( 'NONE', *, *, #1272, .F. ) ;
#8352=ADVANCED_FACE ( 'NONE', ( #5476 ), #2657, .T. ) ;
#8365=ORIENTED_EDGE ( 'NONE', *, *, #3596, .F. ) ;
#8367=EDGE_CURVE ( 'NONE', #10792, #5917, #2585, .T. ) ;
#8375=LINE ( 'NONE', #7326, #4183 ) ;
#8377=ADVANCED_FACE ( 'NONE', ( #3662 ), #7479, .T. ) ;
#8391=CARTESIAN_POINT ( 'NONE',  ( 2.499999999999998668, -4.916402349214439305, -20.41639017900864772 ) ) ;
#8396=ADVANCED_FACE ( 'NONE', ( #4844 ), #1090, .F. ) ;
#8399=AXIS2_PLACEMENT_3D ( 'NONE', #10062, #2421, #11908 ) ;
#8412=CARTESIAN_POINT ( 'NONE',  ( 4.999999999999999112, 0.000000000000000000, 0.000000000000000000 ) ) ;
#8415=DIRECTION ( 'NONE',  ( 0.000000000000000000, 0.000000000000000000, 1.000000000000000000 ) ) ;
#8435=VERTEX_POINT ( 'NONE', #8664 ) ;
#8453=DIRECTION ( 'NONE',  ( 0.000000000000000000, -0.8660254037844433705, 0.4999999999999920064 ) ) ;
#8460=EDGE_CURVE ( 'NONE', #3361, #11522, #11776, .T. ) ;
#8467=ORIENTED_EDGE ( 'NONE', *, *, #2387, .F. ) ;
#8469=CARTESIAN_POINT ( 'NONE',  ( 4.999999999999999112, 20.41639017900859088, 4.916402349214653356 ) ) ;
#8471=DIRECTION ( 'NONE',  ( 0.000000000000000000, 0.000000000000000000, 1.000000000000000000 ) ) ;
#8476=AXIS2_PLACEMENT_3D ( 'NONE', #10668, #1037, #11467 ) ;
#8493=MANIFOLD_SOLID_BREP ( 'Keyway', #10359 ) ;
#8497=CARTESIAN_POINT ( 'NONE',  ( 4.999999999999999112, 0.000000000000000000, 0.000000000000000000 ) ) ;
#8499=EDGE_LOOP ( 'NONE', ( #7118, #5947, #4835, #6358 ) ) ;
#8507=DIRECTION ( 'NONE',  ( 0.000000000000000000, 0.000000000000000000, 1.000000000000000000 ) ) ;
#8511=ORIENTED_EDGE ( 'NONE', *, *, #1570, .T. ) ;
#8514=DIRECTION ( 'NONE',  ( -1.000000000000000000, -0.000000000000000000, -0.000000000000000000 ) ) ;
#8520=DIRECTION ( 'NONE',  ( -1.000000000000000000, 0.000000000000000000, -0.000000000000000000 ) ) ;
#8521=CARTESIAN_POINT ( 'NONE',  ( 4.999999999999999112, 20.41639017900859088, -4.916402349214653356 ) ) ;
#8526=DIRECTION ( 'NONE',  ( 0.000000000000000000, 0.8660254037844363761, 0.5000000000000041078 ) ) ;
#8527=ORIENTED_EDGE ( 'NONE', *, *, #8367, .F. ) ;
#8532=EDGE_LOOP ( 'NONE', ( #10164, #2135, #4310, #5971 ) ) ;
#8533=EDGE_CURVE ( 'NONE', #9327, #10227, #5023, .T. ) ;
#8537=CARTESIAN_POINT ( 'NONE',  ( 4.999999999999999112, 5.622796541391749336, -13.09267581720861173 ) ) ;
#8546=ORIENTED_EDGE ( 'NONE', *, *, #9103, .F. ) ;
#8547=EDGE_CURVE ( 'NONE', #9803, #1217, #599, .T. ) ;
#8559=VERTEX_POINT ( 'NONE', #9335 ) ;
#8560=VERTEX_POINT ( 'NONE', #2637 ) ;
#8563=CARTESIAN_POINT ( 'NONE',  ( 2.499999999999999556, -15.22291137398912397, -14.46592441914980753 ) ) ;
#8575=ORIENTED_EDGE ( 'NONE', *, *, #2538, .F. ) ;
#8576=LINE ( 'NONE', #6762, #635 ) ;
#8583=AXIS2_PLACEMENT_3D ( 'NONE', #5905, #5079, #1137 ) ;
#8586=DIRECTION ( 'NONE',  ( 0.000000000000000000, 0.000000000000000000, -1.000000000000000000 ) ) ;
#8587=FACE_OUTER_BOUND ( 'NONE', #933, .T. ) ;
#8590=VERTEX_POINT ( 'NONE', #5570 ) ;
#8597=LINE ( 'NONE', #3722, #28 ) ;
#8601=VERTEX_POINT ( 'NONE', #7396 ) ;
#8615=AXIS2_PLACEMENT_3D ( 'NONE', #11713, #9975, #8801 ) ;
#8616=DIRECTION ( 'NONE',  ( -1.000000000000000000, 0.000000000000000000, 0.000000000000000000 ) ) ;
#8622=ORIENTED_EDGE ( 'NONE', *, *, #5424, .F. ) ;
#8633=VECTOR ( 'NONE', #12272, 1000.000000000000000 ) ;
#8636=AXIS2_PLACEMENT_3D ( 'NONE', #7853, #2322, #7146 ) ;
#8640=CARTESIAN_POINT ( 'NONE',  ( 4.999999999999999112, 14.40062958310465469, 8.872489362018239234 ) ) ;
#8642=DIRECTION ( 'NONE',  ( 0.000000000000000000, -1.000000000000000000, -0.000000000000000000 ) ) ;
#8645=CIRCLE ( 'NONE', #5638, 14.24900000001425227 ) ;
#8656=CIRCLE ( 'NONE', #4250, 21.00000000002100009 ) ;
#8657=DIRECTION ( 'NONE',  ( 0.000000000000000000, -0.8660254037844328234, -0.5000000000000101030 ) ) ;
#8664=CARTESIAN_POINT ( 'NONE',  ( 4.999999999999999112, -16.90755573046745752, 6.716513609244448624 ) ) ;
#8684=CARTESIAN_POINT ( 'NONE',  ( 4.999999999999999112, 0.000000000000000000, 0.000000000000000000 ) ) ;
#8696=CARTESIAN_POINT ( 'NONE',  ( 5.000000000000000000, 0.000000000000000000, -1.500000000000000000 ) ) ;
#8706=CARTESIAN_POINT ( 'NONE',  ( 0.000000000000000000, -5.622796541391657854, 13.09267581720864904 ) ) ;
#8712=ORIENTED_EDGE ( 'NONE', *, *, #5544, .T. ) ;
#8726=ORIENTED_EDGE ( 'NONE', *, *, #7797, .T. ) ;
#8739=ORIENTED_EDGE ( 'NONE', *, *, #10535, .T. ) ;
#8750=VERTEX_POINT ( 'NONE', #5832 ) ;
#8754=EDGE_CURVE ( 'NONE', #7347, #6441, #415, .T. ) ;
#8768=DIRECTION ( 'NONE',  ( -1.000000000000000000, 0.000000000000000000, 0.000000000000000000 ) ) ;
#8769=CARTESIAN_POINT ( 'NONE',  ( 4.999999999999999112, 1.676853263448085052, -14.14998813191267857 ) ) ;
#8775=ORIENTED_EDGE ( 'NONE', *, *, #7762, .F. ) ;
#8784=AXIS2_PLACEMENT_3D ( 'NONE', #3018, #4080, #7844 ) ;
#8786=DIRECTION ( 'NONE',  ( -1.000000000000000000, 0.000000000000000000, -0.000000000000000000 ) ) ;
#8790=DIRECTION ( 'NONE',  ( -1.000000000000000000, -0.000000000000000000, -0.000000000000000000 ) ) ;
#8799=EDGE_LOOP ( 'NONE', ( #5398, #10782, #10657, #9224 ) ) ;
#8801=DIRECTION ( 'NONE',  ( 0.000000000000000000, 0.000000000000000000, 1.000000000000000000 ) ) ;
#8803=DIRECTION ( 'NONE',  ( 0.000000000000000000, 0.000000000000000000, 1.000000000000000000 ) ) ;
#8808=DIRECTION ( 'NONE',  ( 0.000000000000000000, -0.5000000000000069944, 0.8660254037844344888 ) ) ;
#8809=EDGE_LOOP ( 'NONE', ( #4979, #6975, #9099, #3105 ) ) ;
#8823=AXIS2_PLACEMENT_3D ( 'NONE', #8684, #107, #7742 ) ;
#8825=CIRCLE ( 'NONE', #11000, 7.200000000007204193 ) ;
#8828=ORIENTED_EDGE ( 'NONE', *, *, #1496, .T. ) ;
#8841=FACE_OUTER_BOUND ( 'NONE', #3020, .T. ) ;
#8842=DIRECTION ( 'NONE',  ( -1.000000000000000000, -0.000000000000000000, 0.000000000000000000 ) ) ;
#8847=CIRCLE ( 'NONE', #4437, 21.00000000002100009 ) ;
#8849=CIRCLE ( 'NONE', #841, 7.200000000007202416 ) ;
#8853=EDGE_CURVE ( 'NONE', #4341, #11321, #4004, .T. ) ;
#8859=CARTESIAN_POINT ( 'NONE',  ( 0.000000000000000000, 0.000000000000000000, 0.000000000000000000 ) ) ;
#8862=DIRECTION ( 'NONE',  ( 0.000000000000000000, 0.000000000000000000, 1.000000000000000000 ) ) ;
#8864=DIRECTION ( 'NONE',  ( 1.000000000000000000, 0.000000000000000000, 0.000000000000000000 ) ) ;
#8878=CARTESIAN_POINT ( 'NONE',  ( 4.999999999999997335, 4.769696007084728073, 1.500000000000000000 ) ) ;
#8891=CARTESIAN_POINT ( 'NONE',  ( 4.999999999999999112, -14.40062958310459251, -8.872489362018340486 ) ) ;
#8902=CARTESIAN_POINT ( 'NONE',  ( 4.999999999999999112, -14.88411597386723351, -8.035066368449358620 ) ) ;
#8905=DIRECTION ( 'NONE',  ( -1.000000000000000000, -0.000000000000000000, 0.000000000000000000 ) ) ;
#8920=CARTESIAN_POINT ( 'NONE',  ( 0.000000000000000000, 11.41582255376072830, 8.527191590521114861 ) ) ;
#8925=CYLINDRICAL_SURFACE ( 'NONE', #4008, 7.200000000007202416 ) ;
#8928=VERTEX_POINT ( 'NONE', #7498 ) ;
#8938=EDGE_CURVE ( 'NONE', #394, #10134, #10804, .T. ) ;
#8954=CARTESIAN_POINT ( 'NONE',  ( 0.000000000000000000, 4.916402349214870071, -20.41639017900854469 ) ) ;
#8956=ORIENTED_EDGE ( 'NONE', *, *, #7910, .T. ) ;
#8967=FACE_OUTER_BOUND ( 'NONE', #7309, .T. ) ;
#8984=CARTESIAN_POINT ( 'NONE',  ( 0.000000000000000000, 0.000000000000000000, 0.000000000000000000 ) ) ;
#9004=ORIENTED_EDGE ( 'NONE', *, *, #1554, .T. ) ;
#9007=( GEOMETRIC_REPRESENTATION_CONTEXT ( 3 ) GLOBAL_UNCERTAINTY_ASSIGNED_CONTEXT ( ( #4393 ) ) GLOBAL_UNIT_ASSIGNED_CONTEXT ( ( #513, #11700, #4267 ) ) REPRESENTATION_CONTEXT ( 'NONE', 'WORKASPACE' ) );
#9012=DIRECTION ( 'NONE',  ( 0.000000000000000000, 0.000000000000000000, -1.000000000000000000 ) ) ;
#9015=AXIS2_PLACEMENT_3D ( 'NONE', #4520, #894, #8526 ) ;
#9020=AXIS2_PLACEMENT_3D ( 'NONE', #779, #11228, #205 ) ;
#9022=LINE ( 'NONE', #8769, #439 ) ;
#9025=CARTESIAN_POINT ( 'NONE',  ( 0.000000000000000000, 0.000000000000000000, 0.000000000000000000 ) ) ;
#9031=VERTEX_POINT ( 'NONE', #9686 ) ;
#9036=CIRCLE ( 'NONE', #9441, 7.200000000007203305 ) ;
#9037=VECTOR ( 'NONE', #8034, 1000.000000000000000 ) ;
#9039=DIRECTION ( 'NONE',  ( 1.000000000000000000, -0.000000000000000000, 0.000000000000000000 ) ) ;
#9043=CIRCLE ( 'NONE', #435, 14.24900000001425227 ) ;
#9049=ORIENTED_EDGE ( 'NONE', *, *, #7592, .T. ) ;
#9051=ORIENTED_EDGE ( 'NONE', *, *, #7095, .T. ) ;
#9056=DIRECTION ( 'NONE',  ( 0.000000000000000000, -0.8660254037844328234, -0.5000000000000099920 ) ) ;
#9060=EDGE_CURVE ( 'NONE', #3460, #11522, #976, .T. ) ;
#9076=LINE ( 'NONE', #4242, #1365 ) ;
#9086=DIRECTION ( 'NONE',  ( -1.000000000000000000, -0.000000000000000000, 0.000000000000000000 ) ) ;
#9088=CARTESIAN_POINT ( 'NONE',  ( 4.999999999999999112, -14.14998813191270877, 1.676853263447836584 ) ) ;
#9094=VERTEX_POINT ( 'NONE', #7802 ) ;
#9099=ORIENTED_EDGE ( 'NONE', *, *, #6529, .F. ) ;
#9103=EDGE_CURVE ( 'NONE', #10134, #3361, #229, .T. ) ;
#9114=DIRECTION ( 'NONE',  ( -1.000000000000000000, -0.000000000000000000, 0.000000000000000000 ) ) ;
#9116=DIRECTION ( 'NONE',  ( -1.000000000000000000, -0.000000000000000000, -0.000000000000000000 ) ) ;
#9117=CARTESIAN_POINT ( 'NONE',  ( 4.999999999999997335, 6.799999999999999822, -1.500000000000000000 ) ) ;
#9129=ORIENTED_EDGE ( 'NONE', *, *, #11783, .F. ) ;
#9131=ORIENTED_EDGE ( 'NONE', *, *, #11174, .T. ) ;
#9144=FACE_OUTER_BOUND ( 'NONE', #2460, .T. ) ;
#9145=ORIENTED_EDGE ( 'NONE', *, *, #4227, .F. ) ;
#9150=EDGE_CURVE ( 'NONE', #31, #6433, #9551, .T. ) ;
#9151=EDGE_CURVE ( 'NONE', #9383, #6055, #11398, .T. ) ;
#9159=EDGE_LOOP ( 'NONE', ( #10493, #8278, #5910, #11847 ) ) ;
#9169=CIRCLE ( 'NONE', #11541, 7.200000000007201528 ) ;
#9181=CYLINDRICAL_SURFACE ( 'NONE', #367, 14.24900000001425227 ) ;
#9187=AXIS2_PLACEMENT_3D ( 'NONE', #2337, #8057, #1154 ) ;
#9188=DIRECTION ( 'NONE',  ( 0.000000000000000000, -1.000000000000000000, -1.047444401652940007E-14 ) ) ;
#9197=FACE_OUTER_BOUND ( 'NONE', #8123, .T. ) ;
#9204=CIRCLE ( 'NONE', #2812, 5.000000000000000000 ) ;
#9221=CARTESIAN_POINT ( 'NONE',  ( 4.999999999999999112, -14.40062958310471686, 8.872489362018137982 ) ) ;
#9224=ORIENTED_EDGE ( 'NONE', *, *, #9917, .F. ) ;
#9225=DIRECTION ( 'NONE',  ( -1.000000000000000000, 0.000000000000000000, 0.000000000000000000 ) ) ;
#9227=ADVANCED_FACE ( 'NONE', ( #5104 ), #6160, .F. ) ;
#9232=EDGE_CURVE ( 'NONE', #10549, #3417, #2616, .T. ) ;
#9235=CIRCLE ( 'NONE', #10414, 14.24900000001425227 ) ;
#9242=ORIENTED_EDGE ( 'NONE', *, *, #3860, .T. ) ;
#9243=DIRECTION ( 'NONE',  ( -1.000000000000000000, 0.000000000000000000, 0.000000000000000000 ) ) ;
#9252=DIRECTION ( 'NONE',  ( 0.000000000000000000, 0.000000000000000000, -1.000000000000000000 ) ) ;
#9260=EDGE_CURVE ( 'NONE', #8560, #9354, #2226, .T. ) ;
#9266=VECTOR ( 'NONE', #9703, 1000.000000000000000 ) ;
#9274=CYLINDRICAL_SURFACE ( 'NONE', #12004, 7.200000000007200640 ) ;
#9278=DIRECTION ( 'NONE',  ( 1.000000000000000000, 0.000000000000000000, 0.000000000000000000 ) ) ;
#9292=ORIENTED_EDGE ( 'NONE', *, *, #8853, .T. ) ;
#9297=EDGE_CURVE ( 'NONE', #10309, #9806, #1823, .T. ) ;
#9299=CYLINDRICAL_SURFACE ( 'NONE', #7233, 21.00000000002100009 ) ;
#9301=ADVANCED_FACE ( 'NONE', ( #7168 ), #4404, .T. ) ;
#9303=CARTESIAN_POINT ( 'NONE',  ( 0.000000000000000000, 0.000000000000000000, 0.000000000000000000 ) ) ;
#9308=FACE_OUTER_BOUND ( 'NONE', #5989, .T. ) ;
#9310=DIRECTION ( 'NONE',  ( 1.000000000000000000, 0.000000000000000000, 0.000000000000000000 ) ) ;
#9313=EDGE_CURVE ( 'NONE', #9354, #3359, #6834, .T. ) ;
#9317=DIRECTION ( 'NONE',  ( -1.000000000000000000, -0.000000000000000000, 0.000000000000000000 ) ) ;
#9323=ADVANCED_FACE ( 'NONE', ( #401 ), #4283, .T. ) ;
#9327=VERTEX_POINT ( 'NONE', #1340 ) ;
#9330=CARTESIAN_POINT ( 'NONE',  ( 4.999999999999999112, 14.40062958310465469, 8.872489362018239234 ) ) ;
#9335=CARTESIAN_POINT ( 'NONE',  ( 0.000000000000000000, -13.09267581720862950, -5.622796541391702263 ) ) ;
#9341=DIRECTION ( 'NONE',  ( -1.000000000000000000, 0.000000000000000000, -0.000000000000000000 ) ) ;
#9344=DIRECTION ( 'NONE',  ( -1.000000000000000000, -0.000000000000000000, -0.000000000000000000 ) ) ;
#9345=ORIENTED_EDGE ( 'NONE', *, *, #63, .T. ) ;
#9354=VERTEX_POINT ( 'NONE', #2772 ) ;
#9359=ADVANCED_FACE ( 'NONE', ( #2587 ), #9299, .T. ) ;
#9361=CIRCLE ( 'NONE', #3770, 21.00000000002100009 ) ;
#9362=ORIENTED_EDGE ( 'NONE', *, *, #4858, .T. ) ;
#9372=EDGE_CURVE ( 'NONE', #5533, #11913, #9043, .T. ) ;
#9377=CIRCLE ( 'NONE', #8784, 7.200000000007202416 ) ;
#9378=AXIS2_PLACEMENT_3D ( 'NONE', #6693, #9436, #12230 ) ;
#9383=VERTEX_POINT ( 'NONE', #10279 ) ;
#9385=LINE ( 'NONE', #6567, #1475 ) ;
#9388=CARTESIAN_POINT ( 'NONE',  ( 4.999999999999999112, 14.46592441914964766, 15.22291137398927141 ) ) ;
#9390=EDGE_LOOP ( 'NONE', ( #9145, #9821, #10160, #7947 ) ) ;
#9394=CARTESIAN_POINT ( 'NONE',  ( 4.999999999999999112, 16.90755573046745397, 0.4834863907628708102 ) ) ;
#9395=EDGE_LOOP ( 'NONE', ( #4397, #10898, #7022, #2891 ) ) ;
#9396=AXIS2_PLACEMENT_3D ( 'NONE', #7181, #4116, #2169 ) ;
#9397=DIRECTION ( 'NONE',  ( -1.000000000000000000, 0.000000000000000000, 0.000000000000000000 ) ) ;
#9398=CARTESIAN_POINT ( 'NONE',  ( 0.000000000000000000, -14.14998813191271054, 1.676853263447836806 ) ) ;
#9405=CARTESIAN_POINT ( 'NONE',  ( 0.000000000000000000, -1.676853263447787068, -14.14998813191271410 ) ) ;
#9412=CARTESIAN_POINT ( 'NONE',  ( 5.000000000000000000, 0.000000000000000000, 1.500000000000000000 ) ) ;
#9422=ORIENTED_EDGE ( 'NONE', *, *, #2353, .T. ) ;
#9429=VECTOR ( 'NONE', #6142, 1000.000000000000000 ) ;
#9434=EDGE_CURVE ( 'NONE', #10148, #6613, #6348, .T. ) ;
#9436=DIRECTION ( 'NONE',  ( -1.000000000000000000, 0.000000000000000000, -0.000000000000000000 ) ) ;
#9441=AXIS2_PLACEMENT_3D ( 'NONE', #210, #5205, #4030 ) ;
#9442=DIRECTION ( 'NONE',  ( 0.000000000000000000, 0.000000000000000000, 1.000000000000000000 ) ) ;
#9456=VERTEX_POINT ( 'NONE', #8537 ) ;
#9461=AXIS2_PLACEMENT_3D ( 'NONE', #5815, #122, #11248 ) ;
#9468=DIRECTION ( 'NONE',  ( -1.000000000000000000, 0.000000000000000000, 0.000000000000000000 ) ) ;
#9478=EDGE_CURVE ( 'NONE', #3694, #611, #836, .T. ) ;
#9480=CARTESIAN_POINT ( 'NONE',  ( 0.000000000000000000, -14.40062958310471686, 8.872489362018137982 ) ) ;
#9484=ORIENTED_EDGE ( 'NONE', *, *, #7095, .F. ) ;
#9493=CIRCLE ( 'NONE', #7897, 7.200000000007200640 ) ;
#9498=CARTESIAN_POINT ( 'NONE',  ( 4.999999999999999112, -8.527191590520994069, -11.41582255376081889 ) ) ;
#9499=ORIENTED_EDGE ( 'NONE', *, *, #10914, .F. ) ;
#9501=ORIENTED_EDGE ( 'NONE', *, *, #6760, .T. ) ;
#9508=CARTESIAN_POINT ( 'NONE',  ( 4.999999999999999112, -8.872489362018288972, 14.40062958310462271 ) ) ;
#9522=ORIENTED_EDGE ( 'NONE', *, *, #2879, .T. ) ;
#9528=VERTEX_POINT ( 'NONE', #1029 ) ;
#9532=DIRECTION ( 'NONE',  ( -1.000000000000000000, 0.000000000000000000, 0.000000000000000000 ) ) ;
#9534=DIRECTION ( 'NONE',  ( 0.000000000000000000, 0.8660254037844398178, -0.4999999999999980016 ) ) ;
#9547=ORIENTED_EDGE ( 'NONE', *, *, #9989, .T. ) ;
#9548=EDGE_LOOP ( 'NONE', ( #2279, #6711, #2753, #9362 ) ) ;
#9550=DIRECTION ( 'NONE',  ( -1.000000000000000000, 0.000000000000000000, -0.000000000000000000 ) ) ;
#9551=LINE ( 'NONE', #7741, #828 ) ;
#9557=ORIENTED_EDGE ( 'NONE', *, *, #324, .T. ) ;
#9560=CARTESIAN_POINT ( 'NONE',  ( 4.999999999999999112, 0.000000000000000000, 0.000000000000000000 ) ) ;
#9562=LINE ( 'NONE', #8696, #11972 ) ;
#9567=ORIENTED_EDGE ( 'NONE', *, *, #1130, .T. ) ;
#9570=PLANE ( 'NONE',  #9693 ) ;
#9573=AXIS2_PLACEMENT_3D ( 'NONE', #2573, #10268, #4389 ) ;
#9577=FACE_OUTER_BOUND ( 'NONE', #10689, .T. ) ;
#9584=EDGE_CURVE ( 'NONE', #9031, #403, #6860, .T. ) ;
#9587=VERTEX_POINT ( 'NONE', #10469 ) ;
#9588=DIRECTION ( 'NONE',  ( 0.000000000000000000, 0.8660254037844362651, 0.5000000000000038858 ) ) ;
#9600=ADVANCED_FACE ( 'NONE', ( #10714 ), #9669, .T. ) ;
#9610=AXIS2_PLACEMENT_3D ( 'NONE', #1, #888, #3010 ) ;
#9614=CARTESIAN_POINT ( 'NONE',  ( 0.000000000000000000, 16.90755573046746107, -0.4834863907626340551 ) ) ;
#9615=VECTOR ( 'NONE', #4734, 1000.000000000000000 ) ;
#9617=VECTOR ( 'NONE', #11047, 1000.000000000000000 ) ;
#9619=FACE_OUTER_BOUND ( 'NONE', #7040, .T. ) ;
#9627=CARTESIAN_POINT ( 'NONE',  ( 0.000000000000000000, -16.90755573046746463, 0.4834863907625160939 ) ) ;
#9650=VECTOR ( 'NONE', #1888, 1000.000000000000000 ) ;
#9654=CARTESIAN_POINT ( 'NONE',  ( 4.999999999999999112, 16.90755573046746107, -0.4834863907626340551 ) ) ;
#9668=CARTESIAN_POINT ( 'NONE',  ( 0.000000000000000000, 0.000000000000000000, 0.000000000000000000 ) ) ;
#9669=CYLINDRICAL_SURFACE ( 'NONE', #6436, 7.200000000007202416 ) ;
#9675=CARTESIAN_POINT ( 'NONE',  ( 0.000000000000000000, 0.000000000000000000, 5.000000000000000000 ) ) ;
#9678=ORIENTED_EDGE ( 'NONE', *, *, #9060, .F. ) ;
#9686=CARTESIAN_POINT ( 'NONE',  ( 4.999999999999999112, 5.622796541391564595, 13.09267581720868989 ) ) ;
#9688=EDGE_LOOP ( 'NONE', ( #4931, #3159, #6138, #6148 ) ) ;
#9693=AXIS2_PLACEMENT_3D ( 'NONE', #3890, #8642, #1002 ) ;
#9697=ADVANCED_FACE ( 'NONE', ( #5143 ), #10773, .T. ) ;
#9703=DIRECTION ( 'NONE',  ( 0.000000000000000000, 0.000000000000000000, 1.000000000000000000 ) ) ;
#9704=ORIENTED_EDGE ( 'NONE', *, *, #2090, .T. ) ;
#9716=DIRECTION ( 'NONE',  ( -1.000000000000000000, 0.000000000000000000, 0.000000000000000000 ) ) ;
#9719=DIRECTION ( 'NONE',  ( 1.000000000000000000, 0.000000000000000000, 0.000000000000000000 ) ) ;
#9727=DIRECTION ( 'NONE',  ( -1.000000000000000000, 0.000000000000000000, 0.000000000000000000 ) ) ;
#9744=ORIENTED_EDGE ( 'NONE', *, *, #2284, .F. ) ;
#9748=VERTEX_POINT ( 'NONE', #11019 ) ;
#9752=ORIENTED_EDGE ( 'NONE', *, *, #9584, .T. ) ;
#9757=ADVANCED_FACE ( 'NONE', ( #8967 ), #388, .T. ) ;
#9763=VERTEX_POINT ( 'NONE', #6282 ) ;
#9772=CARTESIAN_POINT ( 'NONE',  ( 4.999999999999999112, 8.872489362018189496, 14.40062958310468666 ) ) ;
#9779=VERTEX_POINT ( 'NONE', #1277 ) ;
#9783=CIRCLE ( 'NONE', #4980, 14.24900000001425049 ) ;
#9791=DIRECTION ( 'NONE',  ( 0.000000000000000000, 0.4999999999999950040, 0.8660254037844414832 ) ) ;
#9792=ORIENTED_EDGE ( 'NONE', *, *, #946, .T. ) ;
#9793=LINE ( 'NONE', #5148, #2885 ) ;
#9797=CARTESIAN_POINT ( 'NONE',  ( 4.999999999999999112, 8.527191590521072229, 11.41582255376076027 ) ) ;
#9803=VERTEX_POINT ( 'NONE', #5518 ) ;
#9806=VERTEX_POINT ( 'NONE', #3522 ) ;
#9809=ORIENTED_EDGE ( 'NONE', *, *, #2493, .F. ) ;
#9820=VECTOR ( 'NONE', #7687, 1000.000000000000000 ) ;
#9821=ORIENTED_EDGE ( 'NONE', *, *, #3043, .T. ) ;
#9824=DIRECTION ( 'NONE',  ( 0.000000000000000000, 0.000000000000000000, 1.000000000000000000 ) ) ;
#9834=DIRECTION ( 'NONE',  ( -1.000000000000000000, 0.000000000000000000, 0.000000000000000000 ) ) ;
#9835=EDGE_CURVE ( 'NONE', #6433, #10549, #5647, .T. ) ;
#9841=DIRECTION ( 'NONE',  ( -1.000000000000000000, 0.000000000000000000, -0.000000000000000000 ) ) ;
#9844=DIRECTION ( 'NONE',  ( 0.000000000000000000, 0.000000000000000000, 1.000000000000000000 ) ) ;
#9865=ORIENTED_EDGE ( 'NONE', *, *, #1205, .F. ) ;
#9867=AXIS2_PLACEMENT_3D ( 'NONE', #9025, #446, #11875 ) ;
#9872=DIRECTION ( 'NONE',  ( -1.000000000000000000, -0.000000000000000000, 0.000000000000000000 ) ) ;
#9882=DIRECTION ( 'NONE',  ( 0.000000000000000000, -6.982962677686266711E-15, 1.000000000000000000 ) ) ;
#9884=EDGE_LOOP ( 'NONE', ( #5440, #3471, #1114, #7746 ) ) ;
#9892=DIRECTION ( 'NONE',  ( 1.000000000000000000, -0.000000000000000000, -0.000000000000000000 ) ) ;
#9895=VERTEX_POINT ( 'NONE', #570 ) ;
#9898=CARTESIAN_POINT ( 'NONE',  ( 0.000000000000000000, 15.22291137398942418, -14.46592441914948779 ) ) ;
#9911=VERTEX_POINT ( 'NONE', #5396 ) ;
#9917=EDGE_CURVE ( 'NONE', #2913, #2151, #8645, .T. ) ;
#9921=CARTESIAN_POINT ( 'NONE',  ( 4.999999999999999112, -0.4834863907624570856, -16.90755573046746463 ) ) ;
#9923=DIRECTION ( 'NONE',  ( -1.000000000000000000, -0.000000000000000000, -0.000000000000000000 ) ) ;
#9942=DIRECTION ( 'NONE',  ( -1.000000000000000000, -0.000000000000000000, -0.000000000000000000 ) ) ;
#9950=CARTESIAN_POINT ( 'NONE',  ( 0.000000000000000000, 0.000000000000000000, 0.000000000000000000 ) ) ;
#9956=CIRCLE ( 'NONE', #1764, 7.200000000007204193 ) ;
#9967=DIRECTION ( 'NONE',  ( 1.000000000000000000, -0.000000000000000000, -0.000000000000000000 ) ) ;
#9975=DIRECTION ( 'NONE',  ( -1.000000000000000000, -0.000000000000000000, -0.000000000000000000 ) ) ;
#9982=AXIS2_PLACEMENT_3D ( 'NONE', #7298, #11092, #5587 ) ;
#9984=VECTOR ( 'NONE', #2250, 1000.000000000000000 ) ;
#9989=EDGE_CURVE ( 'NONE', #542, #4490, #5757, .T. ) ;
#9998=( NAMED_UNIT ( * ) SI_UNIT ( $, .STERADIAN. ) SOLID_ANGLE_UNIT ( ) );
#10005=VECTOR ( 'NONE', #2287, 1000.000000000000000 ) ;
#10007=EDGE_CURVE ( 'NONE', #8024, #4406, #136, .T. ) ;
#10027=VERTEX_POINT ( 'NONE', #3896 ) ;
#10043=ADVANCED_FACE ( 'NONE', ( #7716 ), #10570, .T. ) ;
#10047=DIRECTION ( 'NONE',  ( -1.000000000000000000, 0.000000000000000000, -0.000000000000000000 ) ) ;
#10051=VERTEX_POINT ( 'NONE', #8521 ) ;
#10052=DIRECTION ( 'NONE',  ( -1.000000000000000000, 0.000000000000000000, 0.000000000000000000 ) ) ;
#10057=ORIENTED_EDGE ( 'NONE', *, *, #7096, .T. ) ;
#10062=CARTESIAN_POINT ( 'NONE',  ( 4.999999999999999112, -8.872489362018088244, -14.40062958310474883 ) ) ;
#10067=( LENGTH_UNIT ( ) NAMED_UNIT ( * ) SI_UNIT ( .MILLI., .METRE. ) );
#10080=ORIENTED_EDGE ( 'NONE', *, *, #8853, .F. ) ;
#10087=ORIENTED_EDGE ( 'NONE', *, *, #6947, .T. ) ;
#10093=DIRECTION ( 'NONE',  ( 0.000000000000000000, 0.000000000000000000, 1.000000000000000000 ) ) ;
#10094=DIRECTION ( 'NONE',  ( 0.000000000000000000, 0.000000000000000000, -1.000000000000000000 ) ) ;
#10101=ORIENTED_EDGE ( 'NONE', *, *, #499, .F. ) ;
#10105=CARTESIAN_POINT ( 'NONE',  ( 0.000000000000000000, 0.000000000000000000, 0.000000000000000000 ) ) ;
#10106=DIRECTION ( 'NONE',  ( -1.000000000000000000, -0.000000000000000000, -0.000000000000000000 ) ) ;
#10107=ORIENTED_EDGE ( 'NONE', *, *, #7325, .T. ) ;
#10134=VERTEX_POINT ( 'NONE', #9088 ) ;
#10146=DIRECTION ( 'NONE',  ( -1.000000000000000000, -0.000000000000000000, -0.000000000000000000 ) ) ;
#10148=VERTEX_POINT ( 'NONE', #11691 ) ;
#10160=ORIENTED_EDGE ( 'NONE', *, *, #9260, .T. ) ;
#10161=DIRECTION ( 'NONE',  ( -1.000000000000000000, -0.000000000000000000, -0.000000000000000000 ) ) ;
#10164=ORIENTED_EDGE ( 'NONE', *, *, #6372, .T. ) ;
#10189=DIRECTION ( 'NONE',  ( -1.000000000000000000, -0.000000000000000000, -0.000000000000000000 ) ) ;
#10190=CIRCLE ( 'NONE', #5803, 21.00000000002100009 ) ;
#10191=ORIENTED_EDGE ( 'NONE', *, *, #8267, .F. ) ;
#10200=CIRCLE ( 'NONE', #3013, 7.200000000007202416 ) ;
#10202=DIRECTION ( 'NONE',  ( 1.000000000000000000, 0.000000000000000000, 0.000000000000000000 ) ) ;
#10212=CIRCLE ( 'NONE', #11610, 21.00000000002100009 ) ;
#10227=VERTEX_POINT ( 'NONE', #6507 ) ;
#10228=DIRECTION ( 'NONE',  ( 0.000000000000000000, 0.000000000000000000, -1.000000000000000000 ) ) ;
#10245=ORIENTED_EDGE ( 'NONE', *, *, #125, .F. ) ;
#10250=DIRECTION ( 'NONE',  ( -1.000000000000000000, -0.000000000000000000, 0.000000000000000000 ) ) ;
#10252=ORIENTED_EDGE ( 'NONE', *, *, #5802, .F. ) ;
#10253=DIRECTION ( 'NONE',  ( 0.000000000000000000, 0.000000000000000000, 1.000000000000000000 ) ) ;
#10254=CIRCLE ( 'NONE', #11848, 7.200000000007200640 ) ;
#10265=DIRECTION ( 'NONE',  ( -0.000000000000000000, 1.000000000000000000, 0.000000000000000000 ) ) ;
#10268=DIRECTION ( 'NONE',  ( -1.000000000000000000, 0.000000000000000000, 0.000000000000000000 ) ) ;
#10279=CARTESIAN_POINT ( 'NONE',  ( 0.000000000000000000, 4.769696007084728073, -1.500000000000000000 ) ) ;
#10290=DIRECTION ( 'NONE',  ( 0.000000000000000000, 0.000000000000000000, 1.000000000000000000 ) ) ;
#10294=ADVANCED_FACE ( 'NONE', ( #9197 ), #2550, .T. ) ;
#10309=VERTEX_POINT ( 'NONE', #11992 ) ;
#10313=CARTESIAN_POINT ( 'NONE',  ( 4.999999999999999112, 16.90755573046746107, 6.716513609244568528 ) ) ;
#10314=EDGE_LOOP ( 'NONE', ( #9242, #11793, #8511, #5857 ) ) ;
#10323=DIRECTION ( 'NONE',  ( 0.000000000000000000, 0.000000000000000000, 1.000000000000000000 ) ) ;
#10340=ORIENTED_EDGE ( 'NONE', *, *, #10824, .F. ) ;
#10343=DIRECTION ( 'NONE',  ( 0.000000000000000000, -0.5000000000000069944, 0.8660254037844344888 ) ) ;
#10356=ORIENTED_EDGE ( 'NONE', *, *, #3548, .F. ) ;
#10359=CLOSED_SHELL ( 'NONE', ( #4398, #2239, #10701, #1194, #7492, #8396, #9227, #5789, #7765, #7650, #2343, #6274, #5506, #9359, #12331, #9323, #5643, #10294, #3025, #10507, #11572, #8377, #5921, #11570, #7242, #10043, #2872, #4468, #11501, #6994, #8254, #4322, #1898, #1965, #11127, #5801, #7752, #2477, #9757, #8352, #9697, #11965, #7321, #3475, #7726, #4079, #2382, #1836, #5898, #7562, #3939, #11348, #7869, #6177, #2481, #9600, #6151, #9301, #5283, #365, #1048 ) ) ;
#10360=DIRECTION ( 'NONE',  ( -1.000000000000000000, 0.000000000000000000, -0.000000000000000000 ) ) ;
#10362=CARTESIAN_POINT ( 'NONE',  ( 0.000000000000000000, -8.035066368449101049, -14.88411597386737562 ) ) ;
#10367=AXIS2_PLACEMENT_3D ( 'NONE', #2152, #5976, #8164 ) ;
#10370=ORIENTED_EDGE ( 'NONE', *, *, #4095, .T. ) ;
#10373=CYLINDRICAL_SURFACE ( 'NONE', #12198, 21.00000000002100009 ) ;
#10377=ORIENTED_EDGE ( 'NONE', *, *, #8754, .F. ) ;
#10395=VECTOR ( 'NONE', #9892, 1000.000000000000000 ) ;
#10398=DIRECTION ( 'NONE',  ( -1.000000000000000000, 0.000000000000000000, 0.000000000000000000 ) ) ;
#10407=AXIS2_PLACEMENT_3D ( 'NONE', #11720, #6060, #3929 ) ;
#10414=AXIS2_PLACEMENT_3D ( 'NONE', #11508, #4832, #8657 ) ;
#10426=ORIENTED_EDGE ( 'NONE', *, *, #7706, .T. ) ;
#10441=ORIENTED_EDGE ( 'NONE', *, *, #5343, .F. ) ;
#10442=ORIENTED_EDGE ( 'NONE', *, *, #1256, .T. ) ;
#10444=EDGE_CURVE ( 'NONE', #10027, #629, #2364, .T. ) ;
#10451=ORIENTED_EDGE ( 'NONE', *, *, #1680, .T. ) ;
#10459=VERTEX_POINT ( 'NONE', #931 ) ;
#10460=CARTESIAN_POINT ( 'NONE',  ( 0.000000000000000000, 14.88411597386740404, -8.035066368449049534 ) ) ;
#10463=CARTESIAN_POINT ( 'NONE',  ( 2.499999999999999556, 20.41639017900859443, 4.916402349214656020 ) ) ;
#10469=CARTESIAN_POINT ( 'NONE',  ( 0.000000000000000000, -14.46592441914974714, 15.22291137398917193 ) ) ;
#10485=CYLINDRICAL_SURFACE ( 'NONE', #8225, 21.00000000002100009 ) ;
#10493=ORIENTED_EDGE ( 'NONE', *, *, #4809, .F. ) ;
#10500=EDGE_LOOP ( 'NONE', ( #11873, #10252, #6252, #3367 ) ) ;
#10507=ADVANCED_FACE ( 'NONE', ( #3937 ), #4689, .T. ) ;
#10509=EDGE_CURVE ( 'NONE', #5923, #394, #6561, .T. ) ;
#10516=DIRECTION ( 'NONE',  ( 0.000000000000000000, 0.000000000000000000, 1.000000000000000000 ) ) ;
#10522=EDGE_CURVE ( 'NONE', #10459, #3361, #6968, .T. ) ;
#10523=CARTESIAN_POINT ( 'NONE',  ( -10.00000000000000000, 0.000000000000000000, 0.000000000000000000 ) ) ;
#10524=DIRECTION ( 'NONE',  ( 0.000000000000000000, 0.000000000000000000, -1.000000000000000000 ) ) ;
#10535=EDGE_CURVE ( 'NONE', #3677, #1217, #9076, .T. ) ;
#10549=VERTEX_POINT ( 'NONE', #4064 ) ;
#10551=VECTOR ( 'NONE', #9039, 1000.000000000000000 ) ;
#10556=CARTESIAN_POINT ( 'NONE',  ( 0.000000000000000000, -5.950465759858725612, -20.13931372320394786 ) ) ;
#10561=DIRECTION ( 'NONE',  ( -1.000000000000000000, 0.000000000000000000, 0.000000000000000000 ) ) ;
#10564=ORIENTED_EDGE ( 'NONE', *, *, #5544, .F. ) ;
#10566=CIRCLE ( 'NONE', #7577, 14.24900000001425049 ) ;
#10570=CYLINDRICAL_SURFACE ( 'NONE', #2857, 7.200000000007202416 ) ;
#10575=DIRECTION ( 'NONE',  ( 0.000000000000000000, 0.000000000000000000, -1.000000000000000000 ) ) ;
#10576=CARTESIAN_POINT ( 'NONE',  ( 4.999999999999999112, -20.41639017900856246, -4.916402349214799017 ) ) ;
#10590=ORIENTED_EDGE ( 'NONE', *, *, #2207, .T. ) ;
#10603=ORIENTED_EDGE ( 'NONE', *, *, #4109, .T. ) ;
#10604=AXIS2_PLACEMENT_3D ( 'NONE', #1958, #8842, #10516 ) ;
#10607=AXIS2_PLACEMENT_3D ( 'NONE', #8118, #3236, #11715 ) ;
#10613=EDGE_CURVE ( 'NONE', #4341, #4349, #5116, .T. ) ;
#10615=CARTESIAN_POINT ( 'NONE',  ( 4.999999999999999112, 0.000000000000000000, 0.000000000000000000 ) ) ;
#10619=VECTOR ( 'NONE', #3407, 1000.000000000000000 ) ;
#10620=FACE_OUTER_BOUND ( 'NONE', #1117, .T. ) ;
#10621=VECTOR ( 'NONE', #694, 1000.000000000000000 ) ;
#10628=CIRCLE ( 'NONE', #1057, 21.00000000002100009 ) ;
#10629=ORIENTED_EDGE ( 'NONE', *, *, #8547, .F. ) ;
#10631=CIRCLE ( 'NONE', #5239, 14.24900000001425227 ) ;
#10634=ORIENTED_EDGE ( 'NONE', *, *, #1023, .T. ) ;
#10649=VECTOR ( 'NONE', #8768, 1000.000000000000000 ) ;
#10651=LINE ( 'NONE', #6022, #383 ) ;
#10652=CIRCLE ( 'NONE', #9461, 14.24900000001425227 ) ;
#10655=CARTESIAN_POINT ( 'NONE',  ( 0.000000000000000000, -20.41639017900856246, -4.916402349214799017 ) ) ;
#10657=ORIENTED_EDGE ( 'NONE', *, *, #5484, .T. ) ;
#10664=CARTESIAN_POINT ( 'NONE',  ( 4.999999999999999112, 8.035066368449204077, 14.88411597386731877 ) ) ;
#10666=DIRECTION ( 'NONE',  ( -1.000000000000000000, 0.000000000000000000, 0.000000000000000000 ) ) ;
#10667=ORIENTED_EDGE ( 'NONE', *, *, #1027, .T. ) ;
#10668=CARTESIAN_POINT ( 'NONE',  ( 4.999999999999999112, 0.000000000000000000, 0.000000000000000000 ) ) ;
#10674=DIRECTION ( 'NONE',  ( 0.000000000000000000, 0.000000000000000000, -1.000000000000000000 ) ) ;
#10678=CARTESIAN_POINT ( 'NONE',  ( 4.999999999999999112, 14.88411597386740404, -8.035066368449049534 ) ) ;
#10682=ORIENTED_EDGE ( 'NONE', *, *, #3195, .F. ) ;
#10688=CARTESIAN_POINT ( 'NONE',  ( 0.000000000000000000, -15.22291137398912397, -14.46592441914980753 ) ) ;
#10689=EDGE_LOOP ( 'NONE', ( #8956, #7748, #4682, #940 ) ) ;
#10691=CARTESIAN_POINT ( 'NONE',  ( 0.000000000000000000, 0.000000000000000000, 0.000000000000000000 ) ) ;
#10694=DIRECTION ( 'NONE',  ( 0.000000000000000000, 0.000000000000000000, 1.000000000000000000 ) ) ;
#10701=ADVANCED_FACE ( 'NONE', ( #1681 ), #732, .T. ) ;
#10714=FACE_OUTER_BOUND ( 'NONE', #295, .T. ) ;
#10719=ORIENTED_EDGE ( 'NONE', *, *, #7237, .F. ) ;
#10734=CARTESIAN_POINT ( 'NONE',  ( 4.999999999999999112, 14.40062958310465469, -8.872489362018239234 ) ) ;
#10738=EDGE_CURVE ( 'NONE', #420, #4839, #2571, .T. ) ;
#10741=DIRECTION ( 'NONE',  ( -1.000000000000000000, 0.000000000000000000, 0.000000000000000000 ) ) ;
#10754=DIRECTION ( 'NONE',  ( 0.000000000000000000, 0.000000000000000000, 1.000000000000000000 ) ) ;
#10767=ORIENTED_EDGE ( 'NONE', *, *, #4858, .F. ) ;
#10773=CYLINDRICAL_SURFACE ( 'NONE', #3844, 7.200000000007202416 ) ;
#10775=ORIENTED_EDGE ( 'NONE', *, *, #11721, .F. ) ;
#10776=ORIENTED_EDGE ( 'NONE', *, *, #8533, .T. ) ;
#10782=ORIENTED_EDGE ( 'NONE', *, *, #9372, .T. ) ;
#10784=CARTESIAN_POINT ( 'NONE',  ( 4.999999999999999112, 14.14998813191269633, 1.676853263447936726 ) ) ;
#10787=VERTEX_POINT ( 'NONE', #4297 ) ;
#10788=AXIS2_PLACEMENT_3D ( 'NONE', #6319, #4440, #8268 ) ;
#10789=AXIS2_PLACEMENT_3D ( 'NONE', #7448, #12055, #870 ) ;
#10792=VERTEX_POINT ( 'NONE', #7188 ) ;
#10802=DIRECTION ( 'NONE',  ( 1.000000000000000000, 0.000000000000000000, -0.000000000000000000 ) ) ;
#10804=CIRCLE ( 'NONE', #4019, 14.24900000001425227 ) ;
#10809=AXIS2_PLACEMENT_3D ( 'NONE', #10664, #2094, #11518 ) ;
#10813=ORIENTED_EDGE ( 'NONE', *, *, #10007, .T. ) ;
#10814=DIRECTION ( 'NONE',  ( 1.000000000000000000, 0.000000000000000000, 0.000000000000000000 ) ) ;
#10817=CIRCLE ( 'NONE', #1638, 21.00000000002100009 ) ;
#10824=EDGE_CURVE ( 'NONE', #3785, #9031, #1990, .T. ) ;
#10829=VERTEX_POINT ( 'NONE', #3802 ) ;
#10831=FACE_OUTER_BOUND ( 'NONE', #2503, .T. ) ;
#10845=AXIS2_PLACEMENT_3D ( 'NONE', #1506, #4442, #3630 ) ;
#10853=EDGE_CURVE ( 'NONE', #3834, #12241, #10566, .T. ) ;
#10858=CARTESIAN_POINT ( 'NONE',  ( 0.000000000000000000, 0.000000000000000000, 0.000000000000000000 ) ) ;
#10859=VERTEX_POINT ( 'NONE', #2732 ) ;
#10863=ORIENTED_EDGE ( 'NONE', *, *, #2583, .F. ) ;
#10864=DIRECTION ( 'NONE',  ( 0.000000000000000000, 0.000000000000000000, 1.000000000000000000 ) ) ;
#10874=CARTESIAN_POINT ( 'NONE',  ( 4.999999999999999112, 1.676853263447885878, 14.14998813191270166 ) ) ;
#10898=ORIENTED_EDGE ( 'NONE', *, *, #8151, .F. ) ;
#10909=EDGE_LOOP ( 'NONE', ( #5210, #4651, #12200, #11483 ) ) ;
#10914=EDGE_CURVE ( 'NONE', #1609, #3733, #3370, .T. ) ;
#10921=ORIENTED_EDGE ( 'NONE', *, *, #9313, .F. ) ;
#10924=DIRECTION ( 'NONE',  ( -1.000000000000000000, -0.000000000000000000, 0.000000000000000000 ) ) ;
#10927=LINE ( 'NONE', #3319, #9984 ) ;
#10943=AXIS2_PLACEMENT_3D ( 'NONE', #2115, #5936, #7883 ) ;
#10946=EDGE_CURVE ( 'NONE', #2532, #2177, #7691, .T. ) ;
#10952=ORIENTED_EDGE ( 'NONE', *, *, #6389, .F. ) ;
#10963=LINE ( 'NONE', #2338, #7395 ) ;
#10973=ORIENTED_EDGE ( 'NONE', *, *, #9103, .T. ) ;
#10984=ORIENTED_EDGE ( 'NONE', *, *, #11833, .T. ) ;
#10987=PRESENTATION_STYLE_ASSIGNMENT (( #4429 ) ) ;
#10990=VECTOR ( 'NONE', #859, 1000.000000000000000 ) ;
#10993=CIRCLE ( 'NONE', #8615, 21.00000000002100009 ) ;
#10999=CARTESIAN_POINT ( 'NONE',  ( 0.000000000000000000, 6.799999999999999822, -1.500000000000000000 ) ) ;
#11000=AXIS2_PLACEMENT_3D ( 'NONE', #7441, #4617, #3685 ) ;
#11002=LINE ( 'NONE', #11068, #5651 ) ;
#11019=CARTESIAN_POINT ( 'NONE',  ( 0.000000000000000000, 14.14998813191269633, 1.676853263447936726 ) ) ;
#11025=VECTOR ( 'NONE', #10265, 1000.000000000000000 ) ;
#11028=CARTESIAN_POINT ( 'NONE',  ( 2.499999999999999556, 5.950465759859149273, -20.13931372320382351 ) ) ;
#11045=AXIS2_PLACEMENT_3D ( 'NONE', #2690, #743, #8453 ) ;
#11047=DIRECTION ( 'NONE',  ( 1.000000000000000000, -0.000000000000000000, -0.000000000000000000 ) ) ;
#11049=DIRECTION ( 'NONE',  ( -1.000000000000000000, -0.000000000000000000, 0.000000000000000000 ) ) ;
#11054=DIRECTION ( 'NONE',  ( -1.000000000000000000, 0.000000000000000000, 0.000000000000000000 ) ) ;
#11056=ORIENTED_EDGE ( 'NONE', *, *, #4396, .F. ) ;
#11057=CARTESIAN_POINT ( 'NONE',  ( 4.999999999999999112, -0.4834863907626938961, 16.90755573046746107 ) ) ;
#11063=CARTESIAN_POINT ( 'NONE',  ( 0.000000000000000000, 5.622796541391564595, 13.09267581720868989 ) ) ;
#11068=CARTESIAN_POINT ( 'NONE',  ( 2.499999999999998668, -4.916402349214727074, 20.41639017900857667 ) ) ;
#11092=DIRECTION ( 'NONE',  ( -1.000000000000000000, 0.000000000000000000, -0.000000000000000000 ) ) ;
#11103=CARTESIAN_POINT ( 'NONE',  ( 0.000000000000000000, 8.035066368449204077, 14.88411597386731877 ) ) ;
#11111=( NAMED_UNIT ( * ) SI_UNIT ( $, .STERADIAN. ) SOLID_ANGLE_UNIT ( ) );
#11127=ADVANCED_FACE ( 'NONE', ( #648 ), #6525, .T. ) ;
#11139=CYLINDRICAL_SURFACE ( 'NONE', #9573, 7.200000000007202416 ) ;
#11143=DIRECTION ( 'NONE',  ( 0.000000000000000000, -1.000000000000000000, -1.036015409262890124E-14 ) ) ;
#11170=FACE_OUTER_BOUND ( 'NONE', #4962, .T. ) ;
#11171=EDGE_LOOP ( 'NONE', ( #1703, #3556, #12346, #4144 ) ) ;
#11174=EDGE_CURVE ( 'NONE', #4490, #9779, #7417, .T. ) ;
#11176=CARTESIAN_POINT ( 'NONE',  ( 4.999999999999997335, 0.000000000000000000, 5.000000000000000000 ) ) ;
#11182=DIRECTION ( 'NONE',  ( -1.000000000000000000, 0.000000000000000000, 0.000000000000000000 ) ) ;
#11199=LINE ( 'NONE', #7340, #4755 ) ;
#11200=EDGE_LOOP ( 'NONE', ( #5719, #9522, #9484, #1885 ) ) ;
#11202=CARTESIAN_POINT ( 'NONE',  ( 0.000000000000000000, 0.000000000000000000, 1.500000000000000000 ) ) ;
#11225=ORIENTED_EDGE ( 'NONE', *, *, #11406, .T. ) ;
#11228=DIRECTION ( 'NONE',  ( -1.000000000000000000, 0.000000000000000000, 0.000000000000000000 ) ) ;
#11230=EDGE_CURVE ( 'NONE', #10148, #11485, #4020, .T. ) ;
#11248=DIRECTION ( 'NONE',  ( 0.000000000000000000, 1.000000000000000000, 3.491481338843133355E-15 ) ) ;
#11260=DIRECTION ( 'NONE',  ( -1.000000000000000000, -0.000000000000000000, -0.000000000000000000 ) ) ;
#11270=CARTESIAN_POINT ( 'NONE',  ( 4.999999999999999112, 0.000000000000000000, 14.24900000001425227 ) ) ;
#11278=CARTESIAN_POINT ( 'NONE',  ( 4.999999999999999112, -5.622796541391657854, 13.09267581720865259 ) ) ;
#11282=CARTESIAN_POINT ( 'NONE',  ( 4.999999999999999112, 13.09267581720866858, 5.622796541391611669 ) ) ;
#11284=CARTESIAN_POINT ( 'NONE',  ( 0.000000000000000000, -15.22291137398932470, 14.46592441914958904 ) ) ;
#11300=FACE_BOUND ( 'NONE', #5617, .T. ) ;
#11305=CARTESIAN_POINT ( 'NONE',  ( 0.000000000000000000, -11.41582255376066968, -8.527191590521194797 ) ) ;
#11316=VERTEX_POINT ( 'NONE', #3954 ) ;
#11321=VERTEX_POINT ( 'NONE', #10576 ) ;
#11322=DIRECTION ( 'NONE',  ( 1.000000000000000000, 0.000000000000000000, -0.000000000000000000 ) ) ;
#11323=ORIENTED_EDGE ( 'NONE', *, *, #5254, .T. ) ;
#11331=ORIENTED_EDGE ( 'NONE', *, *, #3428, .T. ) ;
#11336=ORIENTED_EDGE ( 'NONE', *, *, #3644, .T. ) ;
#11348=ADVANCED_FACE ( 'NONE', ( #8587 ), #5906, .T. ) ;
#11359=EDGE_CURVE ( 'NONE', #403, #8328, #6219, .T. ) ;
#11363=DIRECTION ( 'NONE',  ( 0.000000000000000000, 0.000000000000000000, 1.000000000000000000 ) ) ;
#11364=CARTESIAN_POINT ( 'NONE',  ( 0.000000000000000000, 14.40062958310465469, -1.672489362011036595 ) ) ;
#11365=ORIENTED_EDGE ( 'NONE', *, *, #1807, .T. ) ;
#11371=CARTESIAN_POINT ( 'NONE',  ( 4.999999999999999112, 14.40062958310465469, -8.872489362018239234 ) ) ;
#11376=MECHANICAL_DESIGN_GEOMETRIC_PRESENTATION_REPRESENTATION('',(#7408),#9007);
#11379=CIRCLE ( 'NONE', #10788, 7.200000000007201528 ) ;
#11389=ORIENTED_EDGE ( 'NONE', *, *, #804, .T. ) ;
#11393=DIRECTION ( 'NONE',  ( 0.000000000000000000, 0.000000000000000000, 1.000000000000000000 ) ) ;
#11395=CIRCLE ( 'NONE', #3651, 14.24900000001425049 ) ;
#11397=CARTESIAN_POINT ( 'NONE',  ( 0.000000000000000000, 0.000000000000000000, 14.24900000001425227 ) ) ;
#11398=CIRCLE ( 'NONE', #1222, 5.000000000000000000 ) ;
#11406=EDGE_CURVE ( 'NONE', #8093, #11316, #9235, .T. ) ;
#11409=FACE_OUTER_BOUND ( 'NONE', #1124, .T. ) ;
#11411=CARTESIAN_POINT ( 'NONE',  ( 0.000000000000000000, 20.41639017900859443, -4.916402349214656020 ) ) ;
#11418=PLANE ( 'NONE',  #5419 ) ;
#11430=EDGE_CURVE ( 'NONE', #11755, #114, #10817, .T. ) ;
#11431=ORIENTED_EDGE ( 'NONE', *, *, #7171, .F. ) ;
#11432=DIRECTION ( 'NONE',  ( 1.000000000000000000, 0.000000000000000000, 0.000000000000000000 ) ) ;
#11441=DIRECTION ( 'NONE',  ( 0.000000000000000000, 0.000000000000000000, -1.000000000000000000 ) ) ;
#11450=LINE ( 'NONE', #7957, #11553 ) ;
#11459=DIRECTION ( 'NONE',  ( -1.000000000000000000, 0.000000000000000000, 0.000000000000000000 ) ) ;
#11460=LINE ( 'NONE', #3032, #7963 ) ;
#11462=CARTESIAN_POINT ( 'NONE',  ( 4.999999999999999112, 0.000000000000000000, 0.000000000000000000 ) ) ;
#11463=ORIENTED_EDGE ( 'NONE', *, *, #1205, .T. ) ;
#11464=ORIENTED_EDGE ( 'NONE', *, *, #11174, .F. ) ;
#11467=DIRECTION ( 'NONE',  ( 0.000000000000000000, 0.000000000000000000, 1.000000000000000000 ) ) ;
#11483=ORIENTED_EDGE ( 'NONE', *, *, #4109, .F. ) ;
#11485=VERTEX_POINT ( 'NONE', #2197 ) ;
#11486=CARTESIAN_POINT ( 'NONE',  ( 4.999999999999999112, 8.035066368449204077, 14.88411597386731877 ) ) ;
#11494=DIRECTION ( 'NONE',  ( 0.000000000000000000, 0.000000000000000000, -1.000000000000000000 ) ) ;
#11501=ADVANCED_FACE ( 'NONE', ( #9144 ), #1319, .T. ) ;
#11503=CARTESIAN_POINT ( 'NONE',  ( 2.499999999999998668, -15.22291137398932470, 14.46592441914958904 ) ) ;
#11504=CARTESIAN_POINT ( 'NONE',  ( 0.000000000000000000, -14.88411597386734897, 8.035066368449154339 ) ) ;
#11505=EDGE_CURVE ( 'NONE', #2177, #9383, #1453, .T. ) ;
#11507=CARTESIAN_POINT ( 'NONE',  ( 0.000000000000000000, 0.000000000000000000, 0.000000000000000000 ) ) ;
#11508=CARTESIAN_POINT ( 'NONE',  ( 0.000000000000000000, 0.000000000000000000, 0.000000000000000000 ) ) ;
#11509=EDGE_LOOP ( 'NONE', ( #11977, #6484, #3096, #10984 ) ) ;
#11512=ORIENTED_EDGE ( 'NONE', *, *, #4661, .T. ) ;
#11518=DIRECTION ( 'NONE',  ( 0.000000000000000000, 0.000000000000000000, 1.000000000000000000 ) ) ;
#11519=ORIENTED_EDGE ( 'NONE', *, *, #3413, .F. ) ;
#11520=ORIENTED_EDGE ( 'NONE', *, *, #4781, .T. ) ;
#11521=CARTESIAN_POINT ( 'NONE',  ( 4.999999999999999112, -16.90755573046745752, -0.4834863907627537372 ) ) ;
#11522=VERTEX_POINT ( 'NONE', #5194 ) ;
#11529=DIRECTION ( 'NONE',  ( 0.000000000000000000, 0.5000000000000008882, -0.8660254037844381525 ) ) ;
#11532=ORIENTED_EDGE ( 'NONE', *, *, #4396, .T. ) ;
#11533=DIRECTION ( 'NONE',  ( -1.000000000000000000, 0.000000000000000000, -0.000000000000000000 ) ) ;
#11541=AXIS2_PLACEMENT_3D ( 'NONE', #4716, #5775, #9534 ) ;
#11545=CARTESIAN_POINT ( 'NONE',  ( -10.00000000000000000, 0.000000000000000000, 0.000000000000000000 ) ) ;
#11548=LINE ( 'NONE', #4816, #9650 ) ;
#11553=VECTOR ( 'NONE', #5132, 1000.000000000000000 ) ;
#11561=AXIS2_PLACEMENT_3D ( 'NONE', #5180, #10814, #9012 ) ;
#11563=CYLINDRICAL_SURFACE ( 'NONE', #2983, 7.200000000007202416 ) ;
#11566=EDGE_LOOP ( 'NONE', ( #6006, #8467, #10340, #6761, #3755, #202, #2095, #4171, #7108, #4597, #10245, #2086, #3863, #5164, #6494, #3289, #7737, #10863, #10719, #7745, #5794, #4894, #10080, #2876, #952, #5836, #928, #5730, #4413, #1584, #10629, #11693, #11519, #6799, #2916, #141, #3150, #2509, #12152, #10377, #8112, #9129, #2817, #109, #10441, #5355, #4666, #7129, #9499, #821, #2195, #7487, #4921 ) ) ;
#11570=ADVANCED_FACE ( 'NONE', ( #3697 ), #9274, .T. ) ;
#11572=ADVANCED_FACE ( 'NONE', ( #12245 ), #10373, .T. ) ;
#11580=DIRECTION ( 'NONE',  ( -1.000000000000000000, -0.000000000000000000, -0.000000000000000000 ) ) ;
#11594=DIRECTION ( 'NONE',  ( -1.000000000000000000, 0.000000000000000000, -0.000000000000000000 ) ) ;
#11597=AXIS2_PLACEMENT_3D ( 'NONE', #1297, #5111, #2113 ) ;
#11606=AXIS2_PLACEMENT_3D ( 'NONE', #10105, #1532, #7240 ) ;
#11610=AXIS2_PLACEMENT_3D ( 'NONE', #11462, #8790, #2912 ) ;
#11621=FACE_OUTER_BOUND ( 'NONE', #3975, .T. ) ;
#11628=CARTESIAN_POINT ( 'NONE',  ( 4.999999999999999112, 0.000000000000000000, 0.000000000000000000 ) ) ;
#11639=PLANE ( 'NONE',  #4786 ) ;
#11648=DIRECTION ( 'NONE',  ( -1.000000000000000000, 0.000000000000000000, 0.000000000000000000 ) ) ;
#11656=ORIENTED_EDGE ( 'NONE', *, *, #8255, .T. ) ;
#11669=ORIENTED_EDGE ( 'NONE', *, *, #9151, .T. ) ;
#11678=EDGE_CURVE ( 'NONE', #394, #10459, #4447, .T. ) ;
#11680=AXIS2_PLACEMENT_3D ( 'NONE', #490, #3555, #1498 ) ;
#11683=ORIENTED_EDGE ( 'NONE', *, *, #7763, .F. ) ;
#11691=CARTESIAN_POINT ( 'NONE',  ( 4.999999999999999112, -5.622796541391657854, 13.09267581720865259 ) ) ;
#11692=DIRECTION ( 'NONE',  ( 0.000000000000000000, -1.000000000000000000, -1.047444401652940007E-14 ) ) ;
#11693=ORIENTED_EDGE ( 'NONE', *, *, #725, .F. ) ;
#11700=( NAMED_UNIT ( * ) PLANE_ANGLE_UNIT ( ) SI_UNIT ( $, .RADIAN. ) );
#11713=CARTESIAN_POINT ( 'NONE',  ( 0.000000000000000000, 0.000000000000000000, 0.000000000000000000 ) ) ;
#11715=DIRECTION ( 'NONE',  ( 0.000000000000000000, 0.000000000000000000, 1.000000000000000000 ) ) ;
#11720=CARTESIAN_POINT ( 'NONE',  ( 0.000000000000000000, -14.40062958310459251, -8.872489362018340486 ) ) ;
#11721=EDGE_CURVE ( 'NONE', #661, #1926, #879, .T. ) ;
#11730=ORIENTED_EDGE ( 'NONE', *, *, #7533, .F. ) ;
#11731=CYLINDRICAL_SURFACE ( 'NONE', #4259, 7.200000000007202416 ) ;
#11736=ORIENTED_EDGE ( 'NONE', *, *, #2208, .T. ) ;
#11746=VERTEX_POINT ( 'NONE', #72 ) ;
#11749=AXIS2_PLACEMENT_3D ( 'NONE', #6306, #11049, #11853 ) ;
#11755=VERTEX_POINT ( 'NONE', #126 ) ;
#11764=DIRECTION ( 'NONE',  ( -1.000000000000000000, 0.000000000000000000, 0.000000000000000000 ) ) ;
#11774=DIRECTION ( 'NONE',  ( 0.000000000000000000, 0.000000000000000000, 1.000000000000000000 ) ) ;
#11776=CIRCLE ( 'NONE', #1604, 7.200000000007204193 ) ;
#11783=EDGE_CURVE ( 'NONE', #9763, #1333, #1242, .T. ) ;
#11793=ORIENTED_EDGE ( 'NONE', *, *, #6309, .T. ) ;
#11801=CIRCLE ( 'NONE', #6429, 7.200000000007200640 ) ;
#11802=CARTESIAN_POINT ( 'NONE',  ( 4.999999999999999112, 0.000000000000000000, 0.000000000000000000 ) ) ;
#11810=CIRCLE ( 'NONE', #2635, 7.200000000007200640 ) ;
#11816=ORIENTED_EDGE ( 'NONE', *, *, #1130, .F. ) ;
#11821=ORIENTED_EDGE ( 'NONE', *, *, #8938, .T. ) ;
#11824=CIRCLE ( 'NONE', #7261, 7.200000000007202416 ) ;
#11833=EDGE_CURVE ( 'NONE', #3968, #3546, #8847, .T. ) ;
#11834=CARTESIAN_POINT ( 'NONE',  ( 4.999999999999999112, -14.88411597386723351, -8.035066368449358620 ) ) ;
#11835=CARTESIAN_POINT ( 'NONE',  ( -10.00000000000000000, 0.000000000000000000, 0.000000000000000000 ) ) ;
#11846=DIRECTION ( 'NONE',  ( 0.000000000000000000, 0.000000000000000000, -1.000000000000000000 ) ) ;
#11847=ORIENTED_EDGE ( 'NONE', *, *, #9434, .T. ) ;
#11848=AXIS2_PLACEMENT_3D ( 'NONE', #8287, #5472, #577 ) ;
#11853=DIRECTION ( 'NONE',  ( 0.000000000000000000, 0.000000000000000000, 1.000000000000000000 ) ) ;
#11859=ORIENTED_EDGE ( 'NONE', *, *, #9835, .F. ) ;
#11861=CARTESIAN_POINT ( 'NONE',  ( -10.00000000000000000, 0.000000000000000000, 0.000000000000000000 ) ) ;
#11864=EDGE_CURVE ( 'NONE', #5923, #9911, #11548, .T. ) ;
#11870=CARTESIAN_POINT ( 'NONE',  ( 4.999999999999999112, -14.40062958310459251, -8.872489362018340486 ) ) ;
#11873=ORIENTED_EDGE ( 'NONE', *, *, #7910, .F. ) ;
#11874=ORIENTED_EDGE ( 'NONE', *, *, #449, .T. ) ;
#11875=DIRECTION ( 'NONE',  ( 0.000000000000000000, 0.000000000000000000, -1.000000000000000000 ) ) ;
#11877=ORIENTED_EDGE ( 'NONE', *, *, #2284, .T. ) ;
#11892=ORIENTED_EDGE ( 'NONE', *, *, #2207, .F. ) ;
#11898=CARTESIAN_POINT ( 'NONE',  ( 50.00005079999999680, 0.000000000000000000, 0.000000000000000000 ) ) ;
#11899=DIRECTION ( 'NONE',  ( 0.000000000000000000, 0.000000000000000000, 1.000000000000000000 ) ) ;
#11900=ORIENTED_EDGE ( 'NONE', *, *, #10613, .F. ) ;
#11908=DIRECTION ( 'NONE',  ( 0.000000000000000000, -1.000000000000000000, -1.036015409262890124E-14 ) ) ;
#11909=ORIENTED_EDGE ( 'NONE', *, *, #6760, .F. ) ;
#11913=VERTEX_POINT ( 'NONE', #10874 ) ;
#11915=FACE_OUTER_BOUND ( 'NONE', #10909, .T. ) ;
#11930=LINE ( 'NONE', #8391, #3041 ) ;
#11939=AXIS2_PLACEMENT_3D ( 'NONE', #11103, #9310, #9252 ) ;
#11942=EDGE_CURVE ( 'NONE', #8024, #3084, #10628, .T. ) ;
#11957=CARTESIAN_POINT ( 'NONE',  ( 0.000000000000000000, 0.000000000000000000, 0.000000000000000000 ) ) ;
#11960=CARTESIAN_POINT ( 'NONE',  ( 4.999999999999999112, -20.13931372320393010, 5.950465759858794002 ) ) ;
#11965=ADVANCED_FACE ( 'NONE', ( #4177 ), #8004, .T. ) ;
#11972=VECTOR ( 'NONE', #4929, 1000.000000000000000 ) ;
#11977=ORIENTED_EDGE ( 'NONE', *, *, #1680, .F. ) ;
#11992=CARTESIAN_POINT ( 'NONE',  ( 0.000000000000000000, 13.09267581720874674, -5.622796541391427816 ) ) ;
#11995=ORIENTED_EDGE ( 'NONE', *, *, #3596, .T. ) ;
#12004=AXIS2_PLACEMENT_3D ( 'NONE', #9330, #7279, #5512 ) ;
#12009=EDGE_CURVE ( 'NONE', #3733, #3280, #1647, .T. ) ;
#12016=AXIS2_PLACEMENT_3D ( 'NONE', #11835, #4272, #8862 ) ;
#12027=CYLINDRICAL_SURFACE ( 'NONE', #9982, 14.24900000001425227 ) ;
#12029=EDGE_CURVE ( 'NONE', #3834, #4584, #4225, .T. ) ;
#12031=CARTESIAN_POINT ( 'NONE',  ( 4.999999999999999112, 0.000000000000000000, 0.000000000000000000 ) ) ;
#12034=CARTESIAN_POINT ( 'NONE',  ( 4.999999999999999112, 0.000000000000000000, 0.000000000000000000 ) ) ;
#12038=AXIS2_PLACEMENT_3D ( 'NONE', #8891, #6997, #179 ) ;
#12042=VERTEX_POINT ( 'NONE', #11960 ) ;
#12049=CYLINDRICAL_SURFACE ( 'NONE', #5909, 21.00000000002100009 ) ;
#12055=DIRECTION ( 'NONE',  ( 1.000000000000000000, 0.000000000000000000, 0.000000000000000000 ) ) ;
#12076=AXIS2_PLACEMENT_3D ( 'NONE', #9394, #8520, #5756 ) ;
#12127=EDGE_CURVE ( 'NONE', #1723, #3694, #8172, .T. ) ;
#12129=VECTOR ( 'NONE', #2296, 1000.000000000000000 ) ;
#12138=CARTESIAN_POINT ( 'NONE',  ( 0.000000000000000000, 0.000000000000000000, 0.000000000000000000 ) ) ;
#12143=ORIENTED_EDGE ( 'NONE', *, *, #7171, .T. ) ;
#12152=ORIENTED_EDGE ( 'NONE', *, *, #6701, .F. ) ;
#12155=AXIS2_PLACEMENT_3D ( 'NONE', #10460, #4762, #8586 ) ;
#12160=ORIENTED_EDGE ( 'NONE', *, *, #6091, .F. ) ;
#12165=CIRCLE ( 'NONE', #7591, 7.200000000007202416 ) ;
#12167=DIRECTION ( 'NONE',  ( -1.000000000000000000, -0.000000000000000000, 0.000000000000000000 ) ) ;
#12168=EDGE_CURVE ( 'NONE', #866, #7442, #11395, .T. ) ;
#12170=CARTESIAN_POINT ( 'NONE',  ( -10.00000000000000000, 0.000000000000000000, 0.000000000000000000 ) ) ;
#12177=AXIS2_PLACEMENT_3D ( 'NONE', #6715, #1079, #6577 ) ;
#12191=ORIENTED_EDGE ( 'NONE', *, *, #4580, .T. ) ;
#12193=DIRECTION ( 'NONE',  ( 0.000000000000000000, 0.000000000000000000, 1.000000000000000000 ) ) ;
#12195=AXIS2_PLACEMENT_3D ( 'NONE', #8984, #9872, #5226 ) ;
#12198=AXIS2_PLACEMENT_3D ( 'NONE', #6381, #10189, #7513 ) ;
#12199=VECTOR ( 'NONE', #4665, 1000.000000000000000 ) ;
#12200=ORIENTED_EDGE ( 'NONE', *, *, #11505, .T. ) ;
#12215=DIRECTION ( 'NONE',  ( -1.000000000000000000, -0.000000000000000000, -0.000000000000000000 ) ) ;
#12217=ORIENTED_EDGE ( 'NONE', *, *, #6529, .T. ) ;
#12224=EDGE_LOOP ( 'NONE', ( #10767, #3111, #11900, #9292 ) ) ;
#12230=DIRECTION ( 'NONE',  ( 0.000000000000000000, 0.5000000000000008882, -0.8660254037844381525 ) ) ;
#12241=VERTEX_POINT ( 'NONE', #11282 ) ;
#12242=CARTESIAN_POINT ( 'NONE',  ( 4.999999999999999112, 14.40062958310465469, -1.672489362011036595 ) ) ;
#12245=FACE_OUTER_BOUND ( 'NONE', #10500, .T. ) ;
#12251=VECTOR ( 'NONE', #6527, 1000.000000000000000 ) ;
#12261=DIRECTION ( 'NONE',  ( 1.000000000000000000, 0.000000000000000000, 0.000000000000000000 ) ) ;
#12268=CARTESIAN_POINT ( 'NONE',  ( 4.999999999999999112, 0.000000000000000000, 0.000000000000000000 ) ) ;
#12270=DIRECTION ( 'NONE',  ( 0.000000000000000000, 0.000000000000000000, 1.000000000000000000 ) ) ;
#12272=DIRECTION ( 'NONE',  ( -1.000000000000000000, 0.000000000000000000, 0.000000000000000000 ) ) ;
#12278=CARTESIAN_POINT ( 'NONE',  ( 0.000000000000000000, 14.40062958310465469, -8.872489362018239234 ) ) ;
#12291=ORIENTED_EDGE ( 'NONE', *, *, #7325, .F. ) ;
#12297=CARTESIAN_POINT ( 'NONE',  ( 0.000000000000000000, 1.676853263448085052, -14.14998813191267857 ) ) ;
#12320=CARTESIAN_POINT ( 'NONE',  ( 50.00005079999999680, 0.000000000000000000, 0.000000000000000000 ) ) ;
#12324=CARTESIAN_POINT ( 'NONE',  ( 0.000000000000000000, 8.035066368449411911, -14.88411597386720508 ) ) ;
#12331=ADVANCED_FACE ( 'NONE', ( #5969 ), #7789, .T. ) ;
#12335=ORIENTED_EDGE ( 'NONE', *, *, #4712, .F. ) ;
#12337=CARTESIAN_POINT ( 'NONE',  ( 0.000000000000000000, -8.527191590520994069, -11.41582255376081889 ) ) ;
#12346=ORIENTED_EDGE ( 'NONE', *, *, #3413, .T. ) ;
#12348=CIRCLE ( 'NONE', #7376, 21.00000000002100009 ) ;
#12406=COLOUR_RGB('Off White',0.89,0.88,0.83);
#12407=FILL_AREA_STYLE_COLOUR('',#12406);
#12408=FILL_AREA_STYLE('',(#12407));
#12409=SURFACE_STYLE_FILL_AREA(#12408);
#12410=SURFACE_SIDE_STYLE('',(#12409));
#12411=SURFACE_STYLE_USAGE(.BOTH.,#12410);
#12412=PRESENTATION_STYLE_ASSIGNMENT((#12411));
ENDSEC;
END-ISO-10303-21;
